ISO-10303-21;
HEADER;
FILE_DESCRIPTION (('STEP AP214'),
    '1' );
FILE_NAME ('Snap Open Cable Crossbars 14.step',
    '2026-10-08T22:59:04',
    ( '' ),
    ( '' ),
    'SwSTEP 2.0',
    'SolidWorks 2020',
    '' );
FILE_SCHEMA (( 'AUTOMOTIVE_DESIGN' ));
ENDSEC;

DATA;
#72=B_SPLINE_CURVE_WITH_KNOTS ( 'NONE', 3,
 ( #139012, #19102, #60787, #178213, #62093, #257652, #41274, #180758, #218573, #162488, #79052, #22993, #39989, #157373, #119506, #236866, #137752, #173434, #141618, #102458, #199035, #795, #182040, #58212, #240730, #42515, #122066, #201587, #20411, #3376 ),
 .UNSPECIFIED., .F., .F.,
 ( 4, 2, 2, 2, 2, 2, 2, 2, 2, 2, 2, 2, 2, 2, 4 ),
 ( 0.000000000000000000, 0.0003422764154113359459, 0.0006845528308226718917, 0.001026829246234007729, 0.001369105661645343783, 0.002053658492468013290, 0.002738211323290682796, 0.003080487738702016899, 0.003422764154113351869, 0.003765040569524686406, 0.004107316984936021376, 0.004449593400347355912, 0.004791869815758691316, 0.005134146231170024985, 0.005476422646581360389 ),
 .UNSPECIFIED. ) ;
#207=CARTESIAN_POINT ( 'NONE',  ( -16.81744102076748959, 66.05000000001182059, -82.17310748452439384 ) ) ;
#228=DIRECTION ( 'NONE',  ( -1.073024830501117725E-15, 6.982962677686266711E-15, -1.000000000000000000 ) ) ;
#241=ORIENTED_EDGE ( 'NONE', *, *, #154688, .T. ) ;
#358=( LENGTH_UNIT ( ) NAMED_UNIT ( * ) SI_UNIT ( .MILLI., .METRE. ) );
#589=AXIS2_PLACEMENT_3D ( 'NONE', #105465, #182495, #185039 ) ;
#732=CARTESIAN_POINT ( 'NONE',  ( -18.40000000000000213, 70.35000000001187459, -90.37310748452433984 ) ) ;
#765=CARTESIAN_POINT ( 'NONE',  ( -18.39999999999999858, 64.52683809664941350, -93.69716141771641560 ) ) ;
#795=CARTESIAN_POINT ( 'NONE',  ( -15.31895204843005054, 66.60346600605788581, -85.11716770535106491 ) ) ;
#851=EDGE_LOOP ( 'NONE', ( #102145, #160499, #222247 ) ) ;
#893=LINE ( 'NONE', #202972, #43304 ) ;
#1018=CARTESIAN_POINT ( 'NONE',  ( -18.40000000000000213, 67.17743825834537574, -78.77310748452437394 ) ) ;
#1082=CARTESIAN_POINT ( 'NONE',  ( -16.92563707711778775, 66.03100930561501514, -82.14234918500042681 ) ) ;
#1273=DIRECTION ( 'NONE',  ( 0.000000000000000000, -1.000000000000000000, -6.789366196018718420E-15 ) ) ;
#1301=B_SPLINE_CURVE_WITH_KNOTS ( 'NONE', 3,
 ( #78150, #179853, #222794, #162864, #237246, #44192, #98978, #200690, #58583, #161581, #61170, #42898, #178584 ),
 .UNSPECIFIED., .F., .F.,
 ( 4, 3, 3, 3, 4 ),
 ( 1.084445006577768341E-16, 1.946463881814499081E-05, 3.922356109944648083E-05, 4.215060953239448225E-05, 4.415117091092920593E-05 ),
 .UNSPECIFIED. ) ;
#1849=FACE_OUTER_BOUND ( 'NONE', #29017, .T. ) ;
#2007=PLANE ( 'NONE',  #146979 ) ;
#2228=EDGE_CURVE ( 'NONE', #64408, #27378, #122959, .T. ) ;
#2319=LINE ( 'NONE', #1018, #54592 ) ;
#2370=CYLINDRICAL_SURFACE ( 'NONE', #81088, 1.749999999999998002 ) ;
#2409=DIRECTION ( 'NONE',  ( -3.035766082959430717E-14, -6.982962677686266711E-15, 1.000000000000000000 ) ) ;
#2425=AXIS2_PLACEMENT_3D ( 'NONE', #153513, #135160, #16531 ) ;
#2477=ADVANCED_FACE ( 'NONE', ( #140792 ), #198191, .F. ) ;
#2545=DIRECTION ( 'NONE',  ( -1.000000000000000000, 0.000000000000000000, 0.000000000000000000 ) ) ;
#2549=DIRECTION ( 'NONE',  ( 1.000000000000000000, 0.000000000000000000, 0.000000000000000000 ) ) ;
#2568=ADVANCED_FACE ( 'NONE', ( #222880 ), #65099, .F. ) ;
#2670=AXIS2_PLACEMENT_3D ( 'NONE', #120402, #242876, #241594 ) ;
#2744=CARTESIAN_POINT ( 'NONE',  ( -16.87036670365548474, 66.01058118071016168, -82.04354736722233099 ) ) ;
#2966=VERTEX_POINT ( 'NONE', #188430 ) ;
#3016=EDGE_CURVE ( 'NONE', #148732, #119515, #66522, .T. ) ;
#3025=DIRECTION ( 'NONE',  ( 0.000000000000000000, -6.982962677686266711E-15, 1.000000000000000000 ) ) ;
#3065=EDGE_CURVE ( 'NONE', #179449, #121302, #233975, .T. ) ;
#3075=VECTOR ( 'NONE', #31390, 1000.000000000000000 ) ;
#3221=DIRECTION ( 'NONE',  ( -0.000000000000000000, -6.982962677686266711E-15, 1.000000000000000000 ) ) ;
#3288=DIRECTION ( 'NONE',  ( 0.000000000000000000, 6.982962677686266711E-15, -1.000000000000000000 ) ) ;
#3376=CARTESIAN_POINT ( 'NONE',  ( -15.75000000000000355, 66.65000000001185754, -86.27310748452437394 ) ) ;
#3416=EDGE_CURVE ( 'NONE', #191238, #119515, #188141, .T. ) ;
#3612=ORIENTED_EDGE ( 'NONE', *, *, #3016, .T. ) ;
#3813=CARTESIAN_POINT ( 'NONE',  ( 20.05000000000002913, 68.75000000001183764, -90.37310748452435405 ) ) ;
#3944=FACE_OUTER_BOUND ( 'NONE', #53028, .T. ) ;
#3975=ORIENTED_EDGE ( 'NONE', *, *, #60651, .T. ) ;
#4301=FACE_OUTER_BOUND ( 'NONE', #156765, .T. ) ;
#4467=CYLINDRICAL_SURFACE ( 'NONE', #252945, 0.1999999999999987899 ) ;
#4617=CARTESIAN_POINT ( 'NONE',  ( -16.93970660449832621, 65.98715860837630487, -90.47082574872992211 ) ) ;
#4700=DIRECTION ( 'NONE',  ( 0.000000000000000000, 1.000000000000000000, 6.982962677686266711E-15 ) ) ;
#4704=EDGE_CURVE ( 'NONE', #24606, #236196, #84216, .T. ) ;
#4848=DIRECTION ( 'NONE',  ( 1.000000000000000000, 0.000000000000000000, 0.000000000000000000 ) ) ;
#4888=VECTOR ( 'NONE', #125605, 1000.000000000000000 ) ;
#5197=PLANE ( 'NONE',  #39129 ) ;
#5626=CARTESIAN_POINT ( 'NONE',  ( -17.27223548803312170, 65.65460260865577879, -80.88950130532087712 ) ) ;
#5664=ORIENTED_EDGE ( 'NONE', *, *, #30064, .F. ) ;
#5756=ORIENTED_EDGE ( 'NONE', *, *, #127109, .T. ) ;
#5854=LINE ( 'NONE', #7143, #179632 ) ;
#5897=CARTESIAN_POINT ( 'NONE',  ( -16.94309007106720344, 66.00777380744186473, -90.41731620196888741 ) ) ;
#6000=ORIENTED_EDGE ( 'NONE', *, *, #134569, .F. ) ;
#6020=CARTESIAN_POINT ( 'NONE',  ( 18.54999999999999716, 52.34166666667851331, -86.27310748452447342 ) ) ;
#6107=EDGE_LOOP ( 'NONE', ( #243201, #94752, #10728, #168857, #239938, #179576, #127777, #247988, #21830, #12390 ) ) ;
#6231=CARTESIAN_POINT ( 'NONE',  ( -16.94389599337535657, 66.00880201025508143, -82.13075228632277458 ) ) ;
#6312=CARTESIAN_POINT ( 'NONE',  ( 23.24999999999999645, 70.35000000001181775, -82.17310748452436542 ) ) ;
#6493=VECTOR ( 'NONE', #161128, 1000.000000000000000 ) ;
#6623=CARTESIAN_POINT ( 'NONE',  ( -18.38639463286148867, 64.51980042617591948, -93.77310748452438816 ) ) ;
#6710=ORIENTED_EDGE ( 'NONE', *, *, #145332, .T. ) ;
#6754=CARTESIAN_POINT ( 'NONE',  ( -21.65000000000000213, 68.75000000001189449, -93.77310748452435973 ) ) ;
#7057=ORIENTED_EDGE ( 'NONE', *, *, #238222, .T. ) ;
#7143=CARTESIAN_POINT ( 'NONE',  ( 20.09999999999999787, 66.25000000001190870, -93.77310748452438816 ) ) ;
#7257=VERTEX_POINT ( 'NONE', #217950 ) ;
#7273=DIRECTION ( 'NONE',  ( 0.2834754621636358940, 0.2834754621636501049, -0.9161240771326873977 ) ) ;
#7805=EDGE_CURVE ( 'NONE', #202204, #247441, #181131, .T. ) ;
#7816=CARTESIAN_POINT ( 'NONE',  ( -18.38817693311004575, 64.51850848411201866, -78.77310748452438816 ) ) ;
#7851=EDGE_CURVE ( 'NONE', #89858, #69398, #83263, .T. ) ;
#7901=PLANE ( 'NONE',  #111991 ) ;
#7929=CARTESIAN_POINT ( 'NONE',  ( -18.34374000495060386, 64.52683809664941350, -93.77310748452440237 ) ) ;
#8052=FACE_OUTER_BOUND ( 'NONE', #114743, .T. ) ;
#8091=CARTESIAN_POINT ( 'NONE',  ( -21.65000000000000213, 65.95000000001181206, -82.17310748452439384 ) ) ;
#8190=DIRECTION ( 'NONE',  ( 1.652117596168391700E-15, -1.000000000000000000, -6.982962677686266711E-15 ) ) ;
#8214=CARTESIAN_POINT ( 'NONE',  ( -17.29838795458362100, 65.62845014206578753, -91.62784876713939752 ) ) ;
#8287=CARTESIAN_POINT ( 'NONE',  ( -16.83558968593868954, 66.05000000001182059, -82.18541267214132517 ) ) ;
#8314=EDGE_CURVE ( 'NONE', #205773, #54224, #101501, .T. ) ;
#8522=CARTESIAN_POINT ( 'NONE',  ( -16.98495255085916611, 65.99443563401705148, -82.15772469074488527 ) ) ;
#8851=ORIENTED_EDGE ( 'NONE', *, *, #153652, .F. ) ;
#9096=( BOUNDED_SURFACE ( )  B_SPLINE_SURFACE ( 3, 2, ( 
 ( #255834, #94234, #231206 ),
 ( #192079, #175117, #34301 ),
 ( #134628, #77231, #236316 ),
 ( #137217, #212911, #216749 ) ),
 .UNSPECIFIED., .F., .F., .T. ) 
 B_SPLINE_SURFACE_WITH_KNOTS ( ( 4, 4 ),
 ( 3, 3 ),
 ( 0.0008258556059633759532, 0.0009616864997632855591 ),
 ( 0.000000000000000000, 1.000000000000000000 ),
 .UNSPECIFIED. ) 
 GEOMETRIC_REPRESENTATION_ITEM ( )  RATIONAL_B_SPLINE_SURFACE ( (
 ( 1.000000000000000000, 0.9152888060719445162, 1.000000000000000000),
 ( 1.000000000000000000, 0.9327727094138025254, 1.000000000000000000),
 ( 1.000000000000000000, 0.9369023509258468385, 1.000000000000000000),
 ( 1.000000000000000000, 0.9246339933864583527, 1.000000000000000000) ) ) 
 REPRESENTATION_ITEM ( '' )  SURFACE ( )  );
#9373=CARTESIAN_POINT ( 'NONE',  ( -20.65000000000000568, 68.75000000001188027, -90.37310748452435405 ) ) ;
#9518=( NAMED_UNIT ( * ) SI_UNIT ( $, .STERADIAN. ) SOLID_ANGLE_UNIT ( ) );
#9859=CARTESIAN_POINT ( 'NONE',  ( 13.22261339317535978, 66.56344716000741357, -87.84515201176407118 ) ) ;
#10053=VERTEX_POINT ( 'NONE', #207 ) ;
#10328=VERTEX_POINT ( 'NONE', #92579 ) ;
#10552=EDGE_CURVE ( 'NONE', #17815, #161815, #1301, .T. ) ;
#10718=VERTEX_POINT ( 'NONE', #246233 ) ;
#10728=ORIENTED_EDGE ( 'NONE', *, *, #60768, .T. ) ;
#10776=ORIENTED_EDGE ( 'NONE', *, *, #141546, .F. ) ;
#10918=ORIENTED_EDGE ( 'NONE', *, *, #158365, .F. ) ;
#10986=FACE_OUTER_BOUND ( 'NONE', #105795, .T. ) ;
#11146=DIRECTION ( 'NONE',  ( -1.000000000000000000, 0.000000000000000000, 0.000000000000000000 ) ) ;
#11151=CARTESIAN_POINT ( 'NONE',  ( 13.54556439290363556, 66.54940788787816075, -87.96691916571599279 ) ) ;
#11173=CARTESIAN_POINT ( 'NONE',  ( -16.93344882324368683, 66.00341123272393418, -82.11008178971945881 ) ) ;
#11199=CARTESIAN_POINT ( 'NONE',  ( -12.25000000000000178, 66.65000000001185754, -86.27310748452437394 ) ) ;
#11228=LINE ( 'NONE', #214548, #60812 ) ;
#11390=CARTESIAN_POINT ( 'NONE',  ( -16.89268316805465986, 66.04827818676963602, -82.16735500597883401 ) ) ;
#11537=CARTESIAN_POINT ( 'NONE',  ( -16.77683809663752257, 66.05416425680770942, -90.35915846542016538 ) ) ;
#11593=VERTEX_POINT ( 'NONE', #191771 ) ;
#11798=CARTESIAN_POINT ( 'NONE',  ( -18.37160782347004329, 64.52438358520949180, -93.77310748452438816 ) ) ;
#11833=DIRECTION ( 'NONE',  ( 0.7071067811865487940, -0.7071067811865462405, -4.216150419019403701E-15 ) ) ;
#12047=EDGE_CURVE ( 'NONE', #169411, #11593, #893, .T. ) ;
#12103=CARTESIAN_POINT ( 'NONE',  ( 13.43663047529820709, 66.55335465531658201, -84.61230102842419853 ) ) ;
#12147=CARTESIAN_POINT ( 'NONE',  ( -16.90138253750126651, 66.05000000001180638, -82.31154477661976898 ) ) ;
#12308=ORIENTED_EDGE ( 'NONE', *, *, #154348, .F. ) ;
#12390=ORIENTED_EDGE ( 'NONE', *, *, #209788, .T. ) ;
#12393=DIRECTION ( 'NONE',  ( -1.652117596168391700E-15, 1.000000000000000000, 6.982962677686266711E-15 ) ) ;
#12470=CARTESIAN_POINT ( 'NONE',  ( -16.94132844910801339, 66.00756324483145931, -82.12690572854207005 ) ) ;
#12597=EDGE_CURVE ( 'NONE', #100605, #205408, #207843, .T. ) ;
#12801=EDGE_LOOP ( 'NONE', ( #25673, #80183, #180954, #10776, #157881 ) ) ;
#12913=( BOUNDED_CURVE ( )  B_SPLINE_CURVE ( 3, ( #237953, #97121, #116728, #115437 ),
 .UNSPECIFIED., .F., .F. ) 
 B_SPLINE_CURVE_WITH_KNOTS ( ( 4, 4 ),
 ( 0.5235987755982449698, 1.570796326794896558 ),
 .UNSPECIFIED. ) 
 CURVE ( )  GEOMETRIC_REPRESENTATION_ITEM ( )  RATIONAL_B_SPLINE_CURVE ( ( 1.000000000000000000, 0.9106836025229499976, 0.9106836025229499976, 1.000000000000000000 ) ) 
 REPRESENTATION_ITEM ( '' )  );
#12966=ADVANCED_FACE ( 'NONE', ( #104515 ), #105802, .T. ) ;
#13268=( BOUNDED_SURFACE ( )  B_SPLINE_SURFACE ( 3, 2, ( 
 ( #30466, #129555, #212940 ),
 ( #34329, #72159, #68297 ),
 ( #48716, #188238, #91708 ),
 ( #252059, #128271, #190840 ) ),
 .UNSPECIFIED., .F., .F., .F. ) 
 B_SPLINE_SURFACE_WITH_KNOTS ( ( 4, 4 ),
 ( 3, 3 ),
 ( 4.712388980384689674, 5.765869716888531116 ),
 ( 0.000000000000000000, 1.000000000000000000 ),
 .UNSPECIFIED. ) 
 GEOMETRIC_REPRESENTATION_ITEM ( )  RATIONAL_B_SPLINE_SURFACE ( (
 ( 1.000000000000000000, 0.7071067811865475727, 1.000000000000000000),
 ( 1.000000000000000000, 0.7953136715913721178, 1.000000000000000000),
 ( 1.000000000000000000, 0.8646876308615152329, 1.000000000000000000),
 ( 1.000000000000000000, 0.8984936768950676500, 1.000000000000000000) ) ) 
 REPRESENTATION_ITEM ( '' )  SURFACE ( )  );
#13369=CARTESIAN_POINT ( 'NONE',  ( 15.66039659514496130, 66.63925083009672790, -85.70853734391710077 ) ) ;
#13414=CARTESIAN_POINT ( 'NONE',  ( -16.89021194854739250, 66.05000000001180638, -82.28053935292003018 ) ) ;
#13734=CARTESIAN_POINT ( 'NONE',  ( -16.93415306273742260, 66.00437773999929902, -82.11305054216397536 ) ) ;
#14013=VERTEX_POINT ( 'NONE', #105501 ) ;
#14060=DIRECTION ( 'NONE',  ( 1.186688945009010077E-16, 1.000000000000000000, 6.982962677686266711E-15 ) ) ;
#14150=ADVANCED_BREP_SHAPE_REPRESENTATION ( '', ( #189925, #2425 ), #156768 ) ;
#14328=ORIENTED_EDGE ( 'NONE', *, *, #81937, .F. ) ;
#14676=CARTESIAN_POINT ( 'NONE',  ( 12.25000000000000000, 66.65000000001185754, -86.27310748452437394 ) ) ;
#14748=CARTESIAN_POINT ( 'NONE',  ( 18.39999999999999503, 64.25000000001179501, -78.77310748452438816 ) ) ;
#14757=VERTEX_POINT ( 'NONE', #54881 ) ;
#14915=AXIS2_PLACEMENT_3D ( 'NONE', #163071, #143474, #165629 ) ;
#15080=DIRECTION ( 'NONE',  ( 1.020425574104004196E-15, -6.982962677686266711E-15, 1.000000000000000000 ) ) ;
#15090=FACE_OUTER_BOUND ( 'NONE', #255646, .T. ) ;
#15091=CARTESIAN_POINT ( 'NONE',  ( -16.81453046979148880, 66.06089771857094206, -90.31138096092139733 ) ) ;
#15126=ORIENTED_EDGE ( 'NONE', *, *, #118529, .T. ) ;
#15273=ORIENTED_EDGE ( 'NONE', *, *, #135923, .F. ) ;
#15470=EDGE_CURVE ( 'NONE', #197810, #215091, #73623, .T. ) ;
#15615=DIRECTION ( 'NONE',  ( 1.000000000000000000, 0.000000000000000000, 0.000000000000000000 ) ) ;
#15638=CARTESIAN_POINT ( 'NONE',  ( -12.29659703204452015, 66.64411154550927563, -86.73446458774640178 ) ) ;
#15826=ORIENTED_EDGE ( 'NONE', *, *, #159015, .F. ) ;
#16366=CARTESIAN_POINT ( 'NONE',  ( -17.04761207306819060, 65.97354912661410253, -90.37310748452436826 ) ) ;
#16385=CYLINDRICAL_SURFACE ( 'NONE', #218507, 0.5000000000000004441 ) ;
#16531=DIRECTION ( 'NONE',  ( 1.000000000000000000, 0.000000000000000000, 0.000000000000000000 ) ) ;
#16927=CARTESIAN_POINT ( 'NONE',  ( -14.00000000000000178, 66.15000000001185754, -86.27310748452437394 ) ) ;
#17231=ORIENTED_EDGE ( 'NONE', *, *, #234512, .T. ) ;
#17265=ADVANCED_FACE ( 'NONE', ( #46031 ), #39882, .T. ) ;
#17424=CARTESIAN_POINT ( 'NONE',  ( 18.39999999999999147, 67.17743825834548943, -93.77310748452437394 ) ) ;
#17437=CARTESIAN_POINT ( 'NONE',  ( -16.91247567987038636, 66.04091731634262885, -90.39438302598703956 ) ) ;
#17465=CARTESIAN_POINT ( 'NONE',  ( -15.55912972643741199, 67.50912972644930221, -90.37310748452436826 ) ) ;
#17471=CARTESIAN_POINT ( 'NONE',  ( 21.13736287352038445, 67.95335762362780940, -82.17310748452437963 ) ) ;
#17571=CARTESIAN_POINT ( 'NONE',  ( -16.85722902420156188, 66.05000000001189164, -90.25756001075384916 ) ) ;
#17815=VERTEX_POINT ( 'NONE', #254188 ) ;
#17822=ORIENTED_EDGE ( 'NONE', *, *, #149436, .F. ) ;
#18080=FACE_OUTER_BOUND ( 'NONE', #117527, .T. ) ;
#18089=AXIS2_PLACEMENT_3D ( 'NONE', #144861, #164450, #108322 ) ;
#18230=ORIENTED_EDGE ( 'NONE', *, *, #129959, .T. ) ;
#18260=VECTOR ( 'NONE', #83739, 999.9999999999998863 ) ;
#18370=PLANE ( 'NONE',  #105758 ) ;
#18437=PLANE ( 'NONE',  #224302 ) ;
#18585=LINE ( 'NONE', #176392, #245324 ) ;
#18604=CARTESIAN_POINT ( 'NONE',  ( 23.04999999999999716, 67.17743825834537574, -78.77310748452437394 ) ) ;
#18672=VECTOR ( 'NONE', #67333, 1000.000000000000000 ) ;
#18691=FACE_OUTER_BOUND ( 'NONE', #249107, .T. ) ;
#18732=DIRECTION ( 'NONE',  ( 1.186688945009009831E-16, 1.000000000000000000, 6.982962677686266711E-15 ) ) ;
#18767=LINE ( 'NONE', #216958, #78950 ) ;
#18863=CARTESIAN_POINT ( 'NONE',  ( -16.96982749440708815, 66.05000000001187743, -89.89832907571251042 ) ) ;
#18956=ORIENTED_EDGE ( 'NONE', *, *, #230496, .T. ) ;
#18987=LINE ( 'NONE', #98486, #63233 ) ;
#19102=CARTESIAN_POINT ( 'NONE',  ( -12.25000000000000000, 66.65000000001184333, -86.15736431725046884 ) ) ;
#19211=EDGE_LOOP ( 'NONE', ( #96614, #53670, #254626, #165549 ) ) ;
#19365=COLOUR_RGB ( '', 0.72549020, 0.75294118, 0.79215686) ;
#19428=FACE_OUTER_BOUND ( 'NONE', #229626, .T. ) ;
#19490=ADVANCED_FACE ( 'NONE', ( #86830 ), #67288, .T. ) ;
#19572=EDGE_CURVE ( 'NONE', #64408, #148732, #91668, .T. ) ;
#19755=ORIENTED_EDGE ( 'NONE', *, *, #7851, .T. ) ;
#19883=EDGE_CURVE ( 'NONE', #52520, #121571, #109955, .T. ) ;
#19911=CARTESIAN_POINT ( 'NONE',  ( -16.86422026484316916, 66.02955263915120554, -90.44089425885137246 ) ) ;
#20164=EDGE_CURVE ( 'NONE', #48436, #41846, #53072, .T. ) ;
#20168=CARTESIAN_POINT ( 'NONE',  ( -16.83558968593870020, 66.05000000001187743, -90.36080229690789167 ) ) ;
#20255=ADVANCED_FACE ( 'NONE', ( #32734 ), #28890, .F. ) ;
#20324=EDGE_LOOP ( 'NONE', ( #200368, #157836, #236761, #201796 ) ) ;
#20411=CARTESIAN_POINT ( 'NONE',  ( -15.75000000000000711, 66.65000000001182912, -86.15883987690827439 ) ) ;
#20699=CARTESIAN_POINT ( 'NONE',  ( -16.93935632781549572, 66.01526950028672047, -82.13344673581407562 ) ) ;
#20730=CARTESIAN_POINT ( 'NONE',  ( -16.97683809663752186, 66.15000000001188596, -89.62074346632789457 ) ) ;
#20757=CARTESIAN_POINT ( 'NONE',  ( -15.52965525596987995, 66.62446189796385454, -87.15323160353352705 ) ) ;
#20782=CARTESIAN_POINT ( 'NONE',  ( -17.01825945287482966, 65.95000000001188312, -90.37310748452438247 ) ) ;
#21027=LINE ( 'NONE', #100500, #32242 ) ;
#21208=ORIENTED_EDGE ( 'NONE', *, *, #126993, .T. ) ;
#21394=CARTESIAN_POINT ( 'NONE',  ( -18.37013991200266005, 64.50025238379981829, -78.73008447400728471 ) ) ;
#21441=FACE_BOUND ( 'NONE', #203036, .T. ) ;
#21473=CARTESIAN_POINT ( 'NONE',  ( -21.65000000000000213, 68.75000000001188027, -90.37310748452435405 ) ) ;
#21628=ORIENTED_EDGE ( 'NONE', *, *, #22438, .T. ) ;
#21830=ORIENTED_EDGE ( 'NONE', *, *, #241961, .T. ) ;
#21967=ORIENTED_EDGE ( 'NONE', *, *, #200141, .T. ) ;
#22011=DIRECTION ( 'NONE',  ( -0.7071067811865487940, -0.7071067811865463515, -4.216150419019404490E-15 ) ) ;
#22151=CYLINDRICAL_SURFACE ( 'NONE', #234411, 1.749999999999998002 ) ;
#22387=ORIENTED_EDGE ( 'NONE', *, *, #38327, .T. ) ;
#22438=EDGE_CURVE ( 'NONE', #56902, #144564, #152663, .T. ) ;
#22524=CARTESIAN_POINT ( 'NONE',  ( 15.74999999999999645, 66.15000000001185754, -86.27310748452437394 ) ) ;
#22623=CARTESIAN_POINT ( 'NONE',  ( -16.92778301347276582, 65.99905508317655745, -82.09458937655523414 ) ) ;
#22942=CARTESIAN_POINT ( 'NONE',  ( -16.94180778212363236, 66.00755694427971321, -90.41892391399113649 ) ) ;
#22993=CARTESIAN_POINT ( 'NONE',  ( -13.54036565897075484, 66.54845833862633242, -84.56923198569380418 ) ) ;
#23500=MECHANICAL_DESIGN_GEOMETRIC_PRESENTATION_REPRESENTATION('',(#115046),#152677);
#23576=VECTOR ( 'NONE', #102056, 1000.000000000000000 ) ;
#23624=CARTESIAN_POINT ( 'NONE',  ( -16.97683809663752186, 66.05000000001187743, -89.62074346632789457 ) ) ;
#23729=CARTESIAN_POINT ( 'NONE',  ( 17.74533788810829904, 65.18150020854101001, -79.83673015947196916 ) ) ;
#23862=ORIENTED_EDGE ( 'NONE', *, *, #133298, .T. ) ;
#23913=CARTESIAN_POINT ( 'NONE',  ( -16.92973740335360944, 66.00749618554500842, -82.11704844932265246 ) ) ;
#24190=CARTESIAN_POINT ( 'NONE',  ( -18.39999999999999858, 64.52683809664941350, -93.72327823605837693 ) ) ;
#24197=ORIENTED_EDGE ( 'NONE', *, *, #43363, .T. ) ;
#24252=ORIENTED_EDGE ( 'NONE', *, *, #169881, .F. ) ;
#24303=ORIENTED_EDGE ( 'NONE', *, *, #22438, .F. ) ;
#24606=VERTEX_POINT ( 'NONE', #256590 ) ;
#24615=DIRECTION ( 'NONE',  ( -0.000000000000000000, -6.982962677686266711E-15, 1.000000000000000000 ) ) ;
#24825=CARTESIAN_POINT ( 'NONE',  ( 18.39999999999999503, 70.35000000001181775, -82.17310748452435121 ) ) ;
#24831=CARTESIAN_POINT ( 'NONE',  ( -18.40000000000000213, 64.51332499825412015, -78.77310748452438816 ) ) ;
#24866=ORIENTED_EDGE ( 'NONE', *, *, #143309, .T. ) ;
#24974=AXIS2_PLACEMENT_3D ( 'NONE', #171981, #251465, #72872 ) ;
#24979=CARTESIAN_POINT ( 'NONE',  ( -16.79140778683509794, 66.05505840115722549, -82.19337025075358838 ) ) ;
#25037=CARTESIAN_POINT ( 'NONE',  ( -18.40000000000000213, 64.52132590001188817, -78.79780070086499677 ) ) ;
#25198=DIRECTION ( 'NONE',  ( 1.000000000000000000, 0.000000000000000000, 0.000000000000000000 ) ) ;
#25283=FACE_BOUND ( 'NONE', #225769, .T. ) ;
#25287=CARTESIAN_POINT ( 'NONE',  ( -16.77431908686106610, 66.05419424549383223, -82.18726826687414189 ) ) ;
#25356=DIRECTION ( 'NONE',  ( 0.2834754621636439431, 0.2834754621636471628, 0.9161240771326858434 ) ) ;
#25494=CARTESIAN_POINT ( 'NONE',  ( -16.93658211146646408, 66.00589133767067551, -90.42740255448006792 ) ) ;
#25673=ORIENTED_EDGE ( 'NONE', *, *, #76762, .F. ) ;
#25918=EDGE_CURVE ( 'NONE', #77679, #110820, #176359, .T. ) ;
#26102=VERTEX_POINT ( 'NONE', #132756 ) ;
#26113=VERTEX_POINT ( 'NONE', #45811 ) ;
#26115=CARTESIAN_POINT ( 'NONE',  ( 15.74999999999999645, 66.65000000001185754, -86.27310748452437394 ) ) ;
#26475=FACE_OUTER_BOUND ( 'NONE', #227144, .T. ) ;
#26497=VERTEX_POINT ( 'NONE', #11199 ) ;
#26540=( NAMED_UNIT ( * ) PLANE_ANGLE_UNIT ( ) SI_UNIT ( $, .RADIAN. ) );
#26770=CARTESIAN_POINT ( 'NONE',  ( -18.39999999999999858, 64.52132590001261292, -93.74841426818372270 ) ) ;
#26872=DIRECTION ( 'NONE',  ( 1.186688945009009831E-16, 1.000000000000000000, 6.982962677686266711E-15 ) ) ;
#27254=EDGE_CURVE ( 'NONE', #139587, #162722, #257837, .T. ) ;
#27378=VERTEX_POINT ( 'NONE', #56096 ) ;
#27523=CARTESIAN_POINT ( 'NONE',  ( -18.34804628011471195, 64.52683809664951298, -93.77310748452438816 ) ) ;
#27574=DIRECTION ( 'NONE',  ( 1.020425574104004196E-15, 6.982962677686266711E-15, -1.000000000000000000 ) ) ;
#27872=CARTESIAN_POINT ( 'NONE',  ( -16.83233564386400971, 66.06977820342729046, -82.29858682104901391 ) ) ;
#27951=DIRECTION ( 'NONE',  ( 0.000000000000000000, 0.000000000000000000, 1.000000000000000000 ) ) ;
#28003=DIRECTION ( 'NONE',  ( 1.000000000000000000, 0.000000000000000000, 0.000000000000000000 ) ) ;
#28005=ORIENTED_EDGE ( 'NONE', *, *, #27254, .F. ) ;
#28107=CARTESIAN_POINT ( 'NONE',  ( -17.11825945287481332, 65.95000000001181206, -82.17310748452439384 ) ) ;
#28219=CARTESIAN_POINT ( 'NONE',  ( -18.40000000000000213, 64.25000000001188027, -90.37310748452439668 ) ) ;
#28452=DIRECTION ( 'NONE',  ( 1.000000000000000000, 0.000000000000000000, 0.000000000000000000 ) ) ;
#28562=PRODUCT ( 'Snap Open Cable Crossbars 14', 'Snap Open Cable Crossbars 14', '', ( #228306 ) ) ;
#28890=CYLINDRICAL_SURFACE ( 'NONE', #73961, 0.9000000000000014655 ) ;
#29017=EDGE_LOOP ( 'NONE', ( #189642, #112689, #236184, #147629 ) ) ;
#29087=EDGE_CURVE ( 'NONE', #48436, #216777, #95623, .T. ) ;
#29168=CARTESIAN_POINT ( 'NONE',  ( -16.82055514392348172, 66.05000000001182059, -82.19990555906684904 ) ) ;
#29220=DIRECTION ( 'NONE',  ( 0.7071067811865463515, -0.7071067811865487940, -5.696443396193425170E-15 ) ) ;
#29446=VECTOR ( 'NONE', #217650, 1000.000000000000000 ) ;
#29807=LINE ( 'NONE', #53177, #50755 ) ;
#29866=AXIS2_PLACEMENT_3D ( 'NONE', #67659, #108082, #175443 ) ;
#29943=ORIENTED_EDGE ( 'NONE', *, *, #117843, .F. ) ;
#29987=VECTOR ( 'NONE', #15080, 1000.000000000000000 ) ;
#30064=EDGE_CURVE ( 'NONE', #76792, #146896, #42739, .T. ) ;
#30107=ORIENTED_EDGE ( 'NONE', *, *, #49437, .F. ) ;
#30170=EDGE_CURVE ( 'NONE', #162722, #64408, #36839, .T. ) ;
#30373=CARTESIAN_POINT ( 'NONE',  ( 14.22916352759893854, 66.54258906972165732, -84.52319157577809960 ) ) ;
#30413=CARTESIAN_POINT ( 'NONE',  ( -16.81744102076748959, 66.05000000001182059, -82.17310748452439384 ) ) ;
#30446=ORIENTED_EDGE ( 'NONE', *, *, #246309, .F. ) ;
#30466=CARTESIAN_POINT ( 'NONE',  ( -17.11825945287482753, 66.05000000001189164, -90.27310748452437394 ) ) ;
#30624=VECTOR ( 'NONE', #47771, 1000.000000000000000 ) ;
#30740=CARTESIAN_POINT ( 'NONE',  ( 13.88302573338718560, 66.54258905524443435, -88.02302351073434750 ) ) ;
#31052=ORIENTED_EDGE ( 'NONE', *, *, #38327, .F. ) ;
#31390=DIRECTION ( 'NONE',  ( 0.000000000000000000, -1.000000000000000000, -6.982962677686266711E-15 ) ) ;
#31467=ORIENTED_EDGE ( 'NONE', *, *, #46531, .T. ) ;
#32242=VECTOR ( 'NONE', #199659, 1000.000000000000000 ) ;
#32368=CARTESIAN_POINT ( 'NONE',  ( -16.81453563122427752, 66.06089979457485128, -82.23484882387907646 ) ) ;
#32607=ORIENTED_EDGE ( 'NONE', *, *, #10552, .T. ) ;
#32734=FACE_OUTER_BOUND ( 'NONE', #39998, .T. ) ;
#32740=ORIENTED_EDGE ( 'NONE', *, *, #231012, .T. ) ;
#32957=CIRCLE ( 'NONE', #66228, 14.30833333333333890 ) ;
#32972=CARTESIAN_POINT ( 'NONE',  ( 12.68104795156995124, 66.60346600605790002, -85.11716770535107912 ) ) ;
#32994=DIRECTION ( 'NONE',  ( 1.000000000000000000, -1.186688945009009831E-16, -8.286604613020806758E-31 ) ) ;
#33130=ORIENTED_EDGE ( 'NONE', *, *, #54571, .T. ) ;
#33209=EDGE_LOOP ( 'NONE', ( #133250, #3975, #176284, #176239 ) ) ;
#33476=B_SPLINE_CURVE_WITH_KNOTS ( 'NONE', 3,
 ( #96403, #155152, #256727, #20757, #59835, #79405, #233394, #158997, #175986, #218921, #238497, #139377, #117278, #114703, #55985, #213802, #199398, #179830, #153886, #37758, #54725, #194271, #255443, #15638, #95141, #174731 ),
 .UNSPECIFIED., .F., .F.,
 ( 4, 2, 2, 2, 2, 2, 2, 2, 2, 2, 2, 2, 4 ),
 ( 0.005476422646581360389, 0.006160811967703572201, 0.006845201288825784013, 0.007187395949386890352, 0.007529590609947995825, 0.007871785270509102164, 0.008213979931070208504, 0.008556174591631314844, 0.008898369252192419449, 0.009240563912753525788, 0.009582758573314632128, 0.01026714789443684134, 0.01095153721555904881 ),
 .UNSPECIFIED. ) ;
#33691=AXIS2_PLACEMENT_3D ( 'NONE', #226338, #247202, #227637 ) ;
#34241=CARTESIAN_POINT ( 'NONE',  ( 15.57250062127604018, 66.62931007840923314, -85.49664235786335098 ) ) ;
#34270=ORIENTED_EDGE ( 'NONE', *, *, #29087, .T. ) ;
#34301=CARTESIAN_POINT ( 'NONE',  ( -16.85718274719404164, 66.02385768539009803, -90.45976115234198289 ) ) ;
#34329=CARTESIAN_POINT ( 'NONE',  ( -17.01764560440456719, 66.05000000001189164, -90.27310748531118634 ) ) ;
#34459=LINE ( 'NONE', #17424, #236532 ) ;
#34582=CARTESIAN_POINT ( 'NONE',  ( 14.11444803880196552, 66.54256847116293727, -88.02319054662473263 ) ) ;
#34667=CARTESIAN_POINT ( 'NONE',  ( -16.83199030136657726, 66.06935196689842371, -90.25070646186692613 ) ) ;
#34682=ORIENTED_EDGE ( 'NONE', *, *, #210966, .F. ) ;
#34737=DIRECTION ( 'NONE',  ( -1.000000000000000000, 0.000000000000000000, -0.000000000000000000 ) ) ;
#34778=CARTESIAN_POINT ( 'NONE',  ( -17.11825945287482753, 65.95000000001188312, -90.37310748452438247 ) ) ;
#34789=CIRCLE ( 'NONE', #188886, 1.500000000000001332 ) ;
#34828=VERTEX_POINT ( 'NONE', #168889 ) ;
#34922=ORIENTED_EDGE ( 'NONE', *, *, #118590, .F. ) ;
#34977=DIRECTION ( 'NONE',  ( 1.073024830501117725E-15, 6.982962677686266711E-15, -1.000000000000000000 ) ) ;
#35270=VECTOR ( 'NONE', #70806, 1000.000000000000000 ) ;
#35629=AXIS2_PLACEMENT_3D ( 'NONE', #183135, #25356, #138815 ) ;
#35756=LINE ( 'NONE', #177835, #178169 ) ;
#35865=CARTESIAN_POINT ( 'NONE',  ( 15.70340296795548518, 66.64411154550927563, -86.73446458774637335 ) ) ;
#36328=CARTESIAN_POINT ( 'NONE',  ( -21.64999999999999858, 66.65000000001191438, -93.77310748452437394 ) ) ;
#36701=EDGE_LOOP ( 'NONE', ( #114808, #209586, #5664, #224072 ) ) ;
#36728=ORIENTED_EDGE ( 'NONE', *, *, #83625, .T. ) ;
#36756=DIRECTION ( 'NONE',  ( 1.000000000000000000, -1.186688945009009831E-16, -8.286604613020806758E-31 ) ) ;
#36839=( BOUNDED_CURVE ( )  B_SPLINE_CURVE ( 3, ( #86970, #165256, #106541, #149569 ),
 .UNSPECIFIED., .F., .T. ) 
 B_SPLINE_CURVE_WITH_KNOTS ( ( 4, 4 ),
 ( 5.733388419619901200, 5.983100554402347449 ),
 .UNSPECIFIED. ) 
 CURVE ( )  GEOMETRIC_REPRESENTATION_ITEM ( )  RATIONAL_B_SPLINE_CURVE ( ( 1.000000000000000000, 0.9948104011409417691, 0.9948104011409417691, 1.000000000000000000 ) ) 
 REPRESENTATION_ITEM ( '' )  );
#37022=ADVANCED_FACE ( 'NONE', ( #174752 ), #75629, .F. ) ;
#37171=CARTESIAN_POINT ( 'NONE',  ( -16.88783316861822215, 66.05000000001187743, -90.27084344254458870 ) ) ;
#37382=CARTESIAN_POINT ( 'NONE',  ( -16.94107738177415712, 65.98576071487524075, -90.47310748452437679 ) ) ;
#37449=ORIENTED_EDGE ( 'NONE', *, *, #113774, .F. ) ;
#37728=PLANE ( 'NONE',  #140326 ) ;
#37758=CARTESIAN_POINT ( 'NONE',  ( -12.93407622233968723, 66.58221053305966564, -87.66572294054749648 ) ) ;
#37995=CARTESIAN_POINT ( 'NONE',  ( 20.73486653747088582, 68.75000000001185185, -93.77310748452435973 ) ) ;
#38182=DIRECTION ( 'NONE',  ( 1.000000000000000000, 0.000000000000000000, 0.000000000000000000 ) ) ;
#38239=DIRECTION ( 'NONE',  ( 1.186688945009010077E-16, 1.000000000000000000, 6.982962677686266711E-15 ) ) ;
#38327=EDGE_CURVE ( 'NONE', #144564, #83024, #175585, .T. ) ;
#38434=CARTESIAN_POINT ( 'NONE',  ( -16.89935556175729658, 66.05000000001187743, -89.88343112163957471 ) ) ;
#38471=CARTESIAN_POINT ( 'NONE',  ( 23.04999999999999716, 67.17743825834548943, -93.77310748452437394 ) ) ;
#38506=CARTESIAN_POINT ( 'NONE',  ( -16.79139129368505223, 66.05505583755018506, -90.35286285169856058 ) ) ;
#38889=LINE ( 'NONE', #54579, #139495 ) ;
#38895=AXIS2_PLACEMENT_3D ( 'NONE', #72919, #251510, #152451 ) ;
#38915=CARTESIAN_POINT ( 'NONE',  ( -15.55912972643740488, 67.50912972644923116, -82.07310748452437110 ) ) ;
#39129=AXIS2_PLACEMENT_3D ( 'NONE', #24825, #161761, #45646 ) ;
#39494=CARTESIAN_POINT ( 'NONE',  ( -16.86379686415369861, 66.02478224075871083, -90.45649737361466691 ) ) ;
#39496=AXIS2_PLACEMENT_3D ( 'NONE', #230018, #224868, #28003 ) ;
#39616=CARTESIAN_POINT ( 'NONE',  ( -18.40000000000000213, 64.51332499825412015, -78.77310748452438816 ) ) ;
#39700=CIRCLE ( 'NONE', #156224, 0.1999999999999987899 ) ;
#39726=CARTESIAN_POINT ( 'NONE',  ( -16.97683809663752186, 66.05000000001182059, -82.92547150272069700 ) ) ;
#39805=CARTESIAN_POINT ( 'NONE',  ( -21.65000000000000213, 66.05000000001187743, -90.27310748452438816 ) ) ;
#39823=VECTOR ( 'NONE', #117593, 1000.000000000000000 ) ;
#39882=( BOUNDED_SURFACE ( )  B_SPLINE_SURFACE ( 3, 2, ( 
 ( #167299, #149014, #111151 ),
 ( #47296, #109849, #70772 ),
 ( #8214, #250643, #190718 ),
 ( #147714, #208962, #189410 ) ),
 .UNSPECIFIED., .F., .F., .T. ) 
 B_SPLINE_SURFACE_WITH_KNOTS ( ( 4, 4 ),
 ( 3, 3 ),
 ( 5.727910411845712702, 5.983100554402349225 ),
 ( 0.000000000000000000, 1.000000000000000000 ),
 .UNSPECIFIED. ) 
 GEOMETRIC_REPRESENTATION_ITEM ( )  RATIONAL_B_SPLINE_SURFACE ( (
 ( 1.000000000000000000, 0.8946697475932264831, 1.000000000000000000),
 ( 1.000000000000000000, 0.9035312726220648960, 1.000000000000000000),
 ( 1.000000000000000000, 0.9104333467450290707, 1.000000000000000000),
 ( 1.000000000000000000, 0.9152888060719445162, 1.000000000000000000) ) ) 
 REPRESENTATION_ITEM ( '' )  SURFACE ( )  );
#39918=LINE ( 'NONE', #176852, #6493 ) ;
#39989=CARTESIAN_POINT ( 'NONE',  ( -13.77083647240106501, 66.54258906972165732, -84.52319157577809960 ) ) ;
#39998=EDGE_LOOP ( 'NONE', ( #117638, #221740, #100877, #223236 ) ) ;
#40070=ORIENTED_EDGE ( 'NONE', *, *, #49437, .T. ) ;
#40150=CARTESIAN_POINT ( 'NONE',  ( -17.71734398241073905, 65.15764277154723061, -79.79796923151879184 ) ) ;
#40268=( BOUNDED_SURFACE ( )  B_SPLINE_SURFACE ( 3, 2, ( 
 ( #40913, #100806, #202521 ),
 ( #241646, #120453, #22623 ),
 ( #102104, #64294, #23913 ),
 ( #103392, #83810, #242922 ) ),
 .UNSPECIFIED., .F., .F., .F. ) 
 B_SPLINE_SURFACE_WITH_KNOTS ( ( 4, 4 ),
 ( 3, 3 ),
 ( 0.0008258556059633768206, 0.0009616864997632838244 ),
 ( 0.000000000000000000, 1.000000000000000000 ),
 .UNSPECIFIED. ) 
 GEOMETRIC_REPRESENTATION_ITEM ( )  RATIONAL_B_SPLINE_SURFACE ( (
 ( 1.000000000000000000, 0.9152888060719408525, 1.000000000000000000),
 ( 1.000000000000000000, 0.9327727094138034136, 1.000000000000000000),
 ( 1.000000000000000000, 0.9369023509258638249, 1.000000000000000000),
 ( 1.000000000000000000, 0.9246339933864352600, 1.000000000000000000) ) ) 
 REPRESENTATION_ITEM ( '' )  SURFACE ( )  );
#40272=ADVANCED_FACE ( 'NONE', ( #42042 ), #101961, .F. ) ;
#40447=FACE_OUTER_BOUND ( 'NONE', #222870, .T. ) ;
#40656=FACE_OUTER_BOUND ( 'NONE', #196836, .T. ) ;
#40692=VECTOR ( 'NONE', #161573, 1000.000000000000000 ) ;
#40871=ORIENTED_EDGE ( 'NONE', *, *, #115526, .F. ) ;
#40913=CARTESIAN_POINT ( 'NONE',  ( -16.87036670365548474, 66.01058118071014746, -82.04354736722233099 ) ) ;
#41176=CARTESIAN_POINT ( 'NONE',  ( -18.40000000000000213, 67.17743825834548943, -93.77310748452437394 ) ) ;
#41274=CARTESIAN_POINT ( 'NONE',  ( -12.48127053791145080, 66.62341902196787657, -85.39616123751244459 ) ) ;
#41315=DIRECTION ( 'NONE',  ( 0.000000000000000000, -6.982962677686266711E-15, 1.000000000000000000 ) ) ;
#41422=CARTESIAN_POINT ( 'NONE',  ( -17.22361732159831504, 65.65484434140937253, -80.89389201039151089 ) ) ;
#41573=CARTESIAN_POINT ( 'NONE',  ( -16.87331047859649757, 66.05000000001182059, -82.17310748452439384 ) ) ;
#41785=ORIENTED_EDGE ( 'NONE', *, *, #107211, .F. ) ;
#41846=VERTEX_POINT ( 'NONE', #172016 ) ;
#41879=CARTESIAN_POINT ( 'NONE',  ( -16.94445028196808778, 66.00793639031412852, -90.41577730610593733 ) ) ;
#42042=FACE_OUTER_BOUND ( 'NONE', #203761, .T. ) ;
#42044=CARTESIAN_POINT ( 'NONE',  ( -16.86757978335471719, 66.03434962097757932, -90.42510283135686677 ) ) ;
#42108=ORIENTED_EDGE ( 'NONE', *, *, #117843, .T. ) ;
#42224=FACE_OUTER_BOUND ( 'NONE', #125149, .T. ) ;
#42272=CARTESIAN_POINT ( 'NONE',  ( -16.88705144915408951, 66.05000000001180638, -82.45408607923690170 ) ) ;
#42315=ADVANCED_FACE ( 'NONE', ( #40656 ), #94463, .F. ) ;
#42476=ORIENTED_EDGE ( 'NONE', *, *, #168813, .T. ) ;
#42478=CARTESIAN_POINT ( 'NONE',  ( -16.94107738177414291, 65.98576071487519812, -82.07310748452438531 ) ) ;
#42515=CARTESIAN_POINT ( 'NONE',  ( -15.66061380678752535, 66.63927620602578372, -85.70918028991766846 ) ) ;
#42672=PRODUCT_DEFINITION_CONTEXT ( 'detailed design', #175775, 'design' ) ;
#42739=LINE ( 'NONE', #182265, #122754 ) ;
#42898=CARTESIAN_POINT ( 'NONE',  ( -16.77732147278574715, 66.05403306743842506, -90.35959872764857437 ) ) ;
#43179=CARTESIAN_POINT ( 'NONE',  ( -16.87786941232801041, 66.04184528586682745, -82.14592168473036793 ) ) ;
#43216=ORIENTED_EDGE ( 'NONE', *, *, #165366, .F. ) ;
#43304=VECTOR ( 'NONE', #222516, 1000.000000000000000 ) ;
#43363=EDGE_CURVE ( 'NONE', #64408, #111618, #104309, .T. ) ;
#43373=CARTESIAN_POINT ( 'NONE',  ( -21.65000000000000213, 68.75000000001182343, -82.17310748452436542 ) ) ;
#43508=CARTESIAN_POINT ( 'NONE',  ( -16.87036670365548474, 66.01058118071014746, -82.04354736722233099 ) ) ;
#43555=FACE_OUTER_BOUND ( 'NONE', #212090, .T. ) ;
#43714=LINE ( 'NONE', #41176, #132303 ) ;
#43724=FACE_OUTER_BOUND ( 'NONE', #246430, .T. ) ;
#43738=CARTESIAN_POINT ( 'NONE',  ( -20.65000000000000568, 70.35000000001187459, -90.37310748452433984 ) ) ;
#44023=EDGE_CURVE ( 'NONE', #11593, #231129, #89514, .T. ) ;
#44101=ORIENTED_EDGE ( 'NONE', *, *, #159015, .T. ) ;
#44192=CARTESIAN_POINT ( 'NONE',  ( -16.78569801330232281, 66.05206626689836469, -90.36619457917686304 ) ) ;
#44270=DIRECTION ( 'NONE',  ( 1.186688945009010077E-16, 1.000000000000000000, 6.982962677686266711E-15 ) ) ;
#44387=EDGE_LOOP ( 'NONE', ( #148783, #78997, #143379, #241, #128822, #42108 ) ) ;
#44576=VECTOR ( 'NONE', #150954, 1000.000000000000000 ) ;
#44787=CARTESIAN_POINT ( 'NONE',  ( -16.94107738177414291, 65.98576071487519812, -82.07310748452438531 ) ) ;
#44832=CARTESIAN_POINT ( 'NONE',  ( -16.93710578446422943, 66.05000000001182059, -82.44191146832372397 ) ) ;
#45212=VECTOR ( 'NONE', #124700, 1000.000000000000000 ) ;
#45304=ORIENTED_EDGE ( 'NONE', *, *, #173356, .F. ) ;
#45527=AXIS2_PLACEMENT_3D ( 'NONE', #231436, #93183, #172776 ) ;
#45540=DIRECTION ( 'NONE',  ( 0.000000000000000000, 6.982962677686266711E-15, -1.000000000000000000 ) ) ;
#45646=DIRECTION ( 'NONE',  ( 1.000000000000000000, 7.492892343619937423E-30, -1.073024830501117725E-15 ) ) ;
#45736=CARTESIAN_POINT ( 'NONE',  ( -16.86379686415369150, 66.02478224075865398, -82.08971759543409519 ) ) ;
#45745=CARTESIAN_POINT ( 'NONE',  ( -16.92989143108098204, 66.05000000001189164, -90.14062360976771515 ) ) ;
#45768=CYLINDRICAL_SURFACE ( 'NONE', #18089, 0.1000000000000028644 ) ;
#45811=CARTESIAN_POINT ( 'NONE',  ( 20.27550659511089037, 66.78395627750300889, -90.37310748452436826 ) ) ;
#45818=AXIS2_PLACEMENT_3D ( 'NONE', #107190, #125483, #128054 ) ;
#45858=DIRECTION ( 'NONE',  ( 0.000000000000000000, 6.982962677686266711E-15, -1.000000000000000000 ) ) ;
#45871=DIRECTION ( 'NONE',  ( 0.000000000000000000, 6.982962677686266711E-15, -1.000000000000000000 ) ) ;
#45960=EDGE_LOOP ( 'NONE', ( #217867, #83058, #71350, #15126, #92098, #167251 ) ) ;
#46031=FACE_OUTER_BOUND ( 'NONE', #12801, .T. ) ;
#46106=CARTESIAN_POINT ( 'NONE',  ( -16.80621392010915471, 66.05779742250406628, -82.21269944994148204 ) ) ;
#46131=CARTESIAN_POINT ( 'NONE',  ( -16.77180007708460963, 66.05000000001187743, -90.38749336556955427 ) ) ;
#46253=EDGE_CURVE ( 'NONE', #77679, #2966, #234801, .T. ) ;
#46489=VECTOR ( 'NONE', #77332, 1000.000000000000000 ) ;
#46531=EDGE_CURVE ( 'NONE', #11593, #169411, #214137, .T. ) ;
#46668=LINE ( 'NONE', #128803, #230294 ) ;
#46866=EDGE_CURVE ( 'NONE', #139023, #211977, #143885, .T. ) ;
#47019=CARTESIAN_POINT ( 'NONE',  ( -18.35235881385853318, 64.52658099229898880, -93.77310748452438816 ) ) ;
#47122=LINE ( 'NONE', #169710, #158245 ) ;
#47178=DIRECTION ( 'NONE',  ( -1.000000000000000000, -0.000000000000000000, -0.000000000000000000 ) ) ;
#47201=LINE ( 'NONE', #105884, #18260 ) ;
#47296=CARTESIAN_POINT ( 'NONE',  ( -17.80356949363740426, 65.12326860301199360, -92.73618050875685981 ) ) ;
#47326=CARTESIAN_POINT ( 'NONE',  ( 15.75000000000000000, 66.65000000001185754, -86.15736431725046884 ) ) ;
#47392=ADVANCED_FACE ( 'NONE', ( #8052 ), #225778, .F. ) ;
#47605=ORIENTED_EDGE ( 'NONE', *, *, #194625, .F. ) ;
#47753=CARTESIAN_POINT ( 'NONE',  ( -16.87242674293849731, 66.05000000001182059, -82.17201723815203707 ) ) ;
#47771=DIRECTION ( 'NONE',  ( 1.000000000000000000, 0.000000000000000000, 0.000000000000000000 ) ) ;
#48128=CARTESIAN_POINT ( 'NONE',  ( -16.97683809663752186, 66.05000000001183480, -82.92547150272069700 ) ) ;
#48290=CARTESIAN_POINT ( 'NONE',  ( 21.72449340488909897, 65.71604372252068060, -82.17310748452439384 ) ) ;
#48436=VERTEX_POINT ( 'NONE', #22524 ) ;
#48516=ORIENTED_EDGE ( 'NONE', *, *, #165366, .T. ) ;
#48625=CARTESIAN_POINT ( 'NONE',  ( 14.45963434102924339, 66.54845833862631821, -84.56923198569378997 ) ) ;
#48645=SURFACE_SIDE_STYLE ('',( #227285 ) ) ;
#48680=ORIENTED_EDGE ( 'NONE', *, *, #76762, .T. ) ;
#48716=CARTESIAN_POINT ( 'NONE',  ( -16.92209698673556062, 66.05000000001189164, -90.31247191747172565 ) ) ;
#49166=DIRECTION ( 'NONE',  ( -1.073024830501117725E-15, -6.982962677686266711E-15, 1.000000000000000000 ) ) ;
#49362=CLOSED_SHELL ( 'NONE', ( #250430, #92543, #2477, #12966, #239687, #126683, #163600, #226910, #94229, #216332, #185328, #40272, #206463, #231341, #191825, #130510, #47392, #91707, #57887, #193128, #42315, #157460, #68631, #20255, #137924, #126022, #123603, #2568, #185082, #206354, #159569, #254867, #161591, #191092, #37022, #256040, #64070, #115225, #193009, #56992, #88417, #89308, #94726, #96986, #215951, #17265, #49381, #245747, #249818, #160442, #166099, #89587, #19490 ) ) ;
#49381=ADVANCED_FACE ( 'NONE', ( #112533 ), #9096, .T. ) ;
#49437=EDGE_CURVE ( 'NONE', #100605, #91770, #125611, .T. ) ;
#50041=CARTESIAN_POINT ( 'NONE',  ( -17.11825945287482753, 65.95000000001186891, -90.27310748452438816 ) ) ;
#50194=CARTESIAN_POINT ( 'NONE',  ( -16.94445028196807002, 66.00793639031407167, -82.13043766294282477 ) ) ;
#50253=CARTESIAN_POINT ( 'NONE',  ( 18.39999999999999503, 67.17743825834537574, -78.77310748452437394 ) ) ;
#50605=ORIENTED_EDGE ( 'NONE', *, *, #50610, .F. ) ;
#50610=EDGE_CURVE ( 'NONE', #217324, #228701, #47122, .T. ) ;
#50755=VECTOR ( 'NONE', #71487, 1000.000000000000000 ) ;
#51021=VERTEX_POINT ( 'NONE', #188922 ) ;
#51055=CARTESIAN_POINT ( 'NONE',  ( -23.25000000000000355, 70.35000000001187459, -90.37310748452433984 ) ) ;
#51168=CARTESIAN_POINT ( 'NONE',  ( 15.51872946208854920, 66.62341902196789079, -85.39616123751245880 ) ) ;
#51210=CARTESIAN_POINT ( 'NONE',  ( -16.92989507731676468, 66.05000000001183480, -82.40560855391422024 ) ) ;
#51877=CARTESIAN_POINT ( 'NONE',  ( -16.89146115310546037, 66.04855675435534579, -82.16828506557017420 ) ) ;
#52061=EDGE_CURVE ( 'NONE', #191238, #51021, #176472, .T. ) ;
#52122=DIRECTION ( 'NONE',  ( 0.000000000000000000, -6.982962677686266711E-15, 1.000000000000000000 ) ) ;
#52336=ORIENTED_EDGE ( 'NONE', *, *, #100259, .F. ) ;
#52464=CARTESIAN_POINT ( 'NONE',  ( 12.26145404764308999, 66.64858632091046786, -86.04276391697545989 ) ) ;
#52477=VECTOR ( 'NONE', #178294, 1000.000000000000000 ) ;
#52495=CARTESIAN_POINT ( 'NONE',  ( -16.80117486205003630, 66.05034273169948733, -82.17425261159890226 ) ) ;
#52520=VERTEX_POINT ( 'NONE', #165234 ) ;
#53028=EDGE_LOOP ( 'NONE', ( #101189, #83162, #199071, #214437, #188747, #154693, #168253, #160914, #236226, #179734, #31052, #41785, #208693, #128114 ) ) ;
#53072=CIRCLE ( 'NONE', #202925, 1.749999999999998002 ) ;
#53091=PLANE ( 'NONE',  #124909 ) ;
#53177=CARTESIAN_POINT ( 'NONE',  ( -16.27683809663751191, 66.65000000001190017, -90.47310748452437679 ) ) ;
#53380=EDGE_LOOP ( 'NONE', ( #98898, #252846, #256733, #173490 ) ) ;
#53670=ORIENTED_EDGE ( 'NONE', *, *, #167003, .T. ) ;
#54114=CARTESIAN_POINT ( 'NONE',  ( 12.84233041328156588, 66.58946139148298471, -87.59041948738348538 ) ) ;
#54131=CARTESIAN_POINT ( 'NONE',  ( -16.93294127766158752, 65.99671989705693420, -82.09320021869514505 ) ) ;
#54195=CARTESIAN_POINT ( 'NONE',  ( -16.80100426158790583, 66.05684947961573528, -90.34016173169030139 ) ) ;
#54224=VERTEX_POINT ( 'NONE', #249740 ) ;
#54551=PLANE ( 'NONE',  #24974 ) ;
#54571=EDGE_CURVE ( 'NONE', #231129, #10053, #104086, .T. ) ;
#54579=CARTESIAN_POINT ( 'NONE',  ( -15.75000000000000355, 66.15000000001185754, -86.27310748452437394 ) ) ;
#54592=VECTOR ( 'NONE', #140552, 1000.000000000000000 ) ;
#54605=DIRECTION ( 'NONE',  ( -0.7071067811865301422, 0.7071067811865648922, 0.000000000000000000 ) ) ;
#54725=CARTESIAN_POINT ( 'NONE',  ( -12.84409460144754078, 66.58931770574392317, -87.59196404257612301 ) ) ;
#54756=( BOUNDED_SURFACE ( )  B_SPLINE_SURFACE ( 3, 2, ( 
 ( #78795, #240464, #39726 ),
 ( #159651, #61834, #60525 ),
 ( #141360, #220886, #140055 ),
 ( #219601, #42272, #44832 ),
 ( #126938, #87786, #207781 ),
 ( #27872, #206474, #107362 ),
 ( #186938, #129510, #209041 ),
 ( #46106, #29168, #8287 ),
 ( #145199, #167376, #128227 ),
 ( #25287, #225998, #124379 ) ),
 .UNSPECIFIED., .F., .F., .F. ) 
 B_SPLINE_SURFACE_WITH_KNOTS ( ( 4, 2, 2, 2, 4 ),
 ( 3, 3 ),
 ( 0.002161241639767248670, 0.002579950749615824400, 0.002789305304540112482, 0.002893982582002256523, 0.002998659859464400564 ),
 ( 0.000000000000000000, 1.000000000000000000 ),
 .UNSPECIFIED. ) 
 GEOMETRIC_REPRESENTATION_ITEM ( )  RATIONAL_B_SPLINE_SURFACE ( (
 ( 1.000000000000000000, 0.7071067811865475727, 1.000000000000000000),
 ( 1.000000000000000000, 0.7632447400665458570, 1.000000000000000000),
 ( 1.000000000000000000, 0.8158073005108548159, 1.000000000000000000),
 ( 1.000000000000000000, 0.8906973462396701180, 1.000000000000000000),
 ( 1.000000000000000000, 0.9149408947804109626, 1.000000000000000000),
 ( 1.000000000000000000, 0.9493368785273814670, 1.000000000000000000),
 ( 1.000000000000000000, 0.9605194247155347531, 1.000000000000000000),
 ( 1.000000000000000000, 0.9803630264782571269, 1.000000000000000000),
 ( 1.000000000000000000, 0.9900844824270105260, 1.000000000000000000),
 ( 1.000000000000000000, 0.9894588281429241849, 1.000000000000000000) ) ) 
 REPRESENTATION_ITEM ( '' )  SURFACE ( )  );
#54804=ORIENTED_EDGE ( 'NONE', *, *, #114999, .T. ) ;
#54881=CARTESIAN_POINT ( 'NONE',  ( 20.05000000000002913, 68.75000000001178080, -82.17310748452436542 ) ) ;
#55460=ORIENTED_EDGE ( 'NONE', *, *, #95168, .F. ) ;
#55466=CARTESIAN_POINT ( 'NONE',  ( 20.27550659511089037, 66.78395627750295205, -82.17310748452437963 ) ) ;
#55706=CARTESIAN_POINT ( 'NONE',  ( -16.88005004766534967, 66.04989949669077021, -82.17277137257562458 ) ) ;
#55788=CARTESIAN_POINT ( 'NONE',  ( 18.39999999999999503, 70.35000000001181775, -82.17310748452435121 ) ) ;
#55985=CARTESIAN_POINT ( 'NONE',  ( -13.77178122865954180, 66.54397173950395938, -88.01190944945868466 ) ) ;
#56096=CARTESIAN_POINT ( 'NONE',  ( -18.40000000000000213, 64.52683809664931402, -82.07310748452439952 ) ) ;
#56221=DIRECTION ( 'NONE',  ( 1.000000000000000000, 0.000000000000000000, 0.000000000000000000 ) ) ;
#56394=LINE ( 'NONE', #60254, #219872 ) ;
#56902=VERTEX_POINT ( 'NONE', #119781 ) ;
#56992=ADVANCED_FACE ( 'NONE', ( #18080 ), #94105, .T. ) ;
#57774=CARTESIAN_POINT ( 'NONE',  ( 15.74999999999999645, 66.15000000001185754, -86.27310748452437394 ) ) ;
#57887=ADVANCED_FACE ( 'NONE', ( #26475 ), #123006, .F. ) ;
#57972=ORIENTED_EDGE ( 'NONE', *, *, #111590, .T. ) ;
#58193=CARTESIAN_POINT ( 'NONE',  ( -18.40000000000000213, 64.25000000001179501, -78.77310748452438816 ) ) ;
#58212=CARTESIAN_POINT ( 'NONE',  ( -15.51798037960204724, 66.62334006147830223, -85.39491493630713137 ) ) ;
#58388=LINE ( 'NONE', #134095, #213376 ) ;
#58583=CARTESIAN_POINT ( 'NONE',  ( -16.77902162784673834, 66.05358074280401581, -90.36111624045503277 ) ) ;
#58795=EDGE_LOOP ( 'NONE', ( #6000, #217118, #104046, #37449, #75145 ) ) ;
#58932=CARTESIAN_POINT ( 'NONE',  ( 16.87683809663749557, 66.05000000001183480, -82.17310748452439384 ) ) ;
#58964=VECTOR ( 'NONE', #237336, 1000.000000000000000 ) ;
#59035=ORIENTED_EDGE ( 'NONE', *, *, #238325, .F. ) ;
#59423=EDGE_CURVE ( 'NONE', #177874, #69398, #90017, .T. ) ;
#59591=EDGE_CURVE ( 'NONE', #179449, #139023, #138120, .T. ) ;
#59644=CARTESIAN_POINT ( 'NONE',  ( -16.87036670365548474, 66.01058118071016168, -82.04354736722233099 ) ) ;
#59774=CARTESIAN_POINT ( 'NONE',  ( -16.94275863006528482, 66.01050395134429039, -82.13141010244780205 ) ) ;
#59801=DIRECTION ( 'NONE',  ( -1.073024830501117725E-15, -6.982962677686266711E-15, 1.000000000000000000 ) ) ;
#59835=CARTESIAN_POINT ( 'NONE',  ( -15.39946565075090312, 66.61046543766514105, -87.34829818013443514 ) ) ;
#59960=EDGE_CURVE ( 'NONE', #2966, #200313, #5854, .T. ) ;
#60254=CARTESIAN_POINT ( 'NONE',  ( 18.39999999999999503, 64.25000000001182343, -82.17310748452439384 ) ) ;
#60261=DIRECTION ( 'NONE',  ( -0.000000000000000000, 6.982962677686266711E-15, -1.000000000000000000 ) ) ;
#60525=CARTESIAN_POINT ( 'NONE',  ( -16.97683810757273193, 66.05000000001182059, -82.78668419698475134 ) ) ;
#60651=EDGE_CURVE ( 'NONE', #10718, #209659, #197553, .T. ) ;
#60714=CARTESIAN_POINT ( 'NONE',  ( -21.65000000000000213, 66.05000000001187743, -90.27310748452438816 ) ) ;
#60719=LINE ( 'NONE', #732, #115128 ) ;
#60768=EDGE_CURVE ( 'NONE', #69456, #253194, #119314, .T. ) ;
#60787=CARTESIAN_POINT ( 'NONE',  ( -12.26136940704872025, 66.64859682587017176, -86.04357704768588633 ) ) ;
#60805=DIRECTION ( 'NONE',  ( -0.5932847527679299127, -0.8049926720990051576, -6.257843056355997642E-15 ) ) ;
#60812=VECTOR ( 'NONE', #110317, 1000.000000000000000 ) ;
#60831=PLANE ( 'NONE',  #187836 ) ;
#60851=EDGE_CURVE ( 'NONE', #139023, #69456, #167535, .T. ) ;
#61033=DIRECTION ( 'NONE',  ( -0.7071067811865463515, 0.7071067811865487940, 4.178957128135655137E-15 ) ) ;
#61103=CARTESIAN_POINT ( 'NONE',  ( -17.11825945287481332, 66.05000000001182059, -82.27310748452437394 ) ) ;
#61127=CARTESIAN_POINT ( 'NONE',  ( -16.88219499860498374, 66.04979357458428524, -90.37379779441707228 ) ) ;
#61170=CARTESIAN_POINT ( 'NONE',  ( -16.77779411503079032, 66.05389855308774827, -90.36005006690454877 ) ) ;
#61253=DIRECTION ( 'NONE',  ( -1.000000000000000000, 0.000000000000000000, -0.000000000000000000 ) ) ;
#61458=EDGE_CURVE ( 'NONE', #205408, #121571, #234452, .T. ) ;
#61501=CARTESIAN_POINT ( 'NONE',  ( 20.73486653747088937, 68.25000000001178080, -82.17310748452437963 ) ) ;
#61715=ORIENTED_EDGE ( 'NONE', *, *, #229780, .F. ) ;
#61811=CARTESIAN_POINT ( 'NONE',  ( -16.78270389226384296, 66.05262738339480677, -82.18190044761291801 ) ) ;
#61834=CARTESIAN_POINT ( 'NONE',  ( -16.89155683852747813, 66.05000000001449223, -82.80047933406495986 ) ) ;
#62093=CARTESIAN_POINT ( 'NONE',  ( -12.33960340485503870, 66.63925083009671368, -85.70853734391708656 ) ) ;
#62423=CARTESIAN_POINT ( 'NONE',  ( -16.87487986503753845, 66.04999244492626076, -90.37313274483764758 ) ) ;
#62557=CARTESIAN_POINT ( 'NONE',  ( -16.77683809663752257, 52.34166666667851331, -86.27310748452447342 ) ) ;
#62675=LINE ( 'NONE', #37995, #80117 ) ;
#62818=CARTESIAN_POINT ( 'NONE',  ( 17.23472005113826810, 65.69211804551103739, -80.97653062445571948 ) ) ;
#62960=ORIENTED_EDGE ( 'NONE', *, *, #118590, .T. ) ;
#63195=CARTESIAN_POINT ( 'NONE',  ( -18.40000000000000213, 70.35000000001187459, -90.37310748452433984 ) ) ;
#63233=VECTOR ( 'NONE', #116820, 1000.000000000000000 ) ;
#63295=ORIENTED_EDGE ( 'NONE', *, *, #2228, .F. ) ;
#63421=LINE ( 'NONE', #243349, #45212 ) ;
#63556=CARTESIAN_POINT ( 'NONE',  ( 18.39999999999997371, 64.52683809664929981, -78.77310748452438816 ) ) ;
#63820=VECTOR ( 'NONE', #115081, 1000.000000000000000 ) ;
#64070=ADVANCED_FACE ( 'NONE', ( #201874 ), #2370, .F. ) ;
#64278=VERTEX_POINT ( 'NONE', #196422 ) ;
#64294=CARTESIAN_POINT ( 'NONE',  ( -16.90202395485847475, 66.03405545546029032, -82.12009376326403753 ) ) ;
#64408=VERTEX_POINT ( 'NONE', #42478 ) ;
#64410=DIRECTION ( 'NONE',  ( 0.000000000000000000, -1.000000000000000000, -6.982962677686266711E-15 ) ) ;
#64896=DIRECTION ( 'NONE',  ( 0.000000000000000000, -1.000000000000000000, -6.982962677686266711E-15 ) ) ;
#65099=PLANE ( 'NONE',  #109925 ) ;
#65160=VECTOR ( 'NONE', #130791, 1000.000000000000000 ) ;
#65335=VERTEX_POINT ( 'NONE', #170555 ) ;
#65403=CARTESIAN_POINT ( 'NONE',  ( -21.64999999999999858, 65.95000000001188312, -90.37310748452438247 ) ) ;
#65661=CARTESIAN_POINT ( 'NONE',  ( 23.24999999999999645, 64.25000000001188027, -90.37310748452438247 ) ) ;
#65891=CARTESIAN_POINT ( 'NONE',  ( -16.93583594267724379, 65.99137656495966553, -90.46371664520363254 ) ) ;
#66068=CARTESIAN_POINT ( 'NONE',  ( -17.01825945287481545, 66.05000000001182059, -82.27310748452437394 ) ) ;
#66228=AXIS2_PLACEMENT_3D ( 'NONE', #62557, #78248, #1273 ) ;
#66229=VERTEX_POINT ( 'NONE', #138431 ) ;
#66256=LINE ( 'NONE', #167952, #93438 ) ;
#66272=CARTESIAN_POINT ( 'NONE',  ( -16.87383368123029825, 66.05000000001187743, -90.37310748452438247 ) ) ;
#66522=( BOUNDED_CURVE ( )  B_SPLINE_CURVE ( 3, ( #50194, #8522, #148034, #28107 ),
 .UNSPECIFIED., .F., .T. ) 
 B_SPLINE_CURVE_WITH_KNOTS ( ( 4, 4 ),
 ( 3.752122642744585068, 4.712388980384675463 ),
 .UNSPECIFIED. ) 
 CURVE ( )  GEOMETRIC_REPRESENTATION_ITEM ( )  RATIONAL_B_SPLINE_CURVE ( ( 1.000000000000000000, 0.9246222802177217481, 0.9246222802177217481, 1.000000000000000000 ) ) 
 REPRESENTATION_ITEM ( '' )  );
#66581=LINE ( 'NONE', #110824, #94762 ) ;
#66603=CARTESIAN_POINT ( 'NONE',  ( -16.89020380669786192, 66.05000000001187743, -90.26569633641385337 ) ) ;
#66895=DIRECTION ( 'NONE',  ( 1.000000000000000000, 0.000000000000000000, 0.000000000000000000 ) ) ;
#66932=PRESENTATION_STYLE_ASSIGNMENT (( #189460 ) ) ;
#66971=CARTESIAN_POINT ( 'NONE',  ( 18.54999999999999716, 67.25000000001183764, -90.37310748452436826 ) ) ;
#67269=CARTESIAN_POINT ( 'NONE',  ( -18.40000000000000213, 64.52683809664939929, -90.41452884076171870 ) ) ;
#67288=CYLINDRICAL_SURFACE ( 'NONE', #33691, 0.1000000000000028644 ) ;
#67333=DIRECTION ( 'NONE',  ( -0.000000000000000000, -6.982962677686266711E-15, 1.000000000000000000 ) ) ;
#67336=CARTESIAN_POINT ( 'NONE',  ( -17.04295772865454239, 65.97510057475034273, -82.17310748452439384 ) ) ;
#67464=DIRECTION ( 'NONE',  ( 0.7071067811865214825, -0.7071067811865735520, 0.000000000000000000 ) ) ;
#67659=CARTESIAN_POINT ( 'NONE',  ( -23.25000000000000355, 64.25000000001190870, -93.77310748452438816 ) ) ;
#67835=CARTESIAN_POINT ( 'NONE',  ( -18.40000000000000213, 64.66825945288661615, -82.17310748452439384 ) ) ;
#68222=FILL_AREA_STYLE_COLOUR ( '', #19365 ) ;
#68258=EDGE_CURVE ( 'NONE', #255984, #89858, #250487, .T. ) ;
#68297=CARTESIAN_POINT ( 'NONE',  ( -17.04295772865474490, 65.97510057475035694, -90.37310748452436826 ) ) ;
#68432=ORIENTED_EDGE ( 'NONE', *, *, #3016, .F. ) ;
#68631=ADVANCED_FACE ( 'NONE', ( #113243 ), #54551, .F. ) ;
#68851=CARTESIAN_POINT ( 'NONE',  ( -16.87331047859651179, 66.05000000001187743, -90.37310748452438247 ) ) ;
#69203=AXIS2_PLACEMENT_3D ( 'NONE', #177195, #78050, #157642 ) ;
#69232=PLANE ( 'NONE',  #166142 ) ;
#69246=CARTESIAN_POINT ( 'NONE',  ( -18.40000000000000213, 64.52683809664938508, -90.37310748452438247 ) ) ;
#69398=VERTEX_POINT ( 'NONE', #210142 ) ;
#69441=ORIENTED_EDGE ( 'NONE', *, *, #188749, .F. ) ;
#69456=VERTEX_POINT ( 'NONE', #221662 ) ;
#69501=LINE ( 'NONE', #109870, #39823 ) ;
#69522=VERTEX_POINT ( 'NONE', #242526 ) ;
#69860=CARTESIAN_POINT ( 'NONE',  ( 15.06592377766031277, 66.58221053305965142, -87.66572294054748227 ) ) ;
#69865=CARTESIAN_POINT ( 'NONE',  ( -18.40000000000000213, 64.66825945288670141, -90.37310748452438247 ) ) ;
#69962=ORIENTED_EDGE ( 'NONE', *, *, #59960, .T. ) ;
#69985=( BOUNDED_CURVE ( )  B_SPLINE_CURVE ( 3, ( #59644, #41422, #40150, #175797 ),
 .UNSPECIFIED., .F., .F. ) 
 B_SPLINE_CURVE_WITH_KNOTS ( ( 4, 4 ),
 ( 0.3000847527772386725, 0.5517402753107893965 ),
 .UNSPECIFIED. ) 
 CURVE ( )  GEOMETRIC_REPRESENTATION_ITEM ( )  RATIONAL_B_SPLINE_CURVE ( ( 1.000000000000000000, 0.9947294176030464508, 0.9947294176030464508, 1.000000000000000000 ) ) 
 REPRESENTATION_ITEM ( '' )  );
#70294=CARTESIAN_POINT ( 'NONE',  ( 18.54999999999999716, 67.25000000001185185, -93.77310748452437394 ) ) ;
#70772=CARTESIAN_POINT ( 'NONE',  ( -17.73285935861198581, 65.14201819622113021, -92.78166929430516063 ) ) ;
#70795=CARTESIAN_POINT ( 'NONE',  ( 13.88638282980484284, 66.54257354752293452, -84.52306561612435587 ) ) ;
#70806=DIRECTION ( 'NONE',  ( 1.186688945009010077E-16, 1.000000000000000000, 6.982962677686266711E-15 ) ) ;
#70839=CARTESIAN_POINT ( 'NONE',  ( -16.97048361161167307, 66.05000000001180638, -82.66422314009398065 ) ) ;
#70991=DIRECTION ( 'NONE',  ( -1.186688945009010077E-16, -1.000000000000000000, -6.982962677686266711E-15 ) ) ;
#71350=ORIENTED_EDGE ( 'NONE', *, *, #4704, .T. ) ;
#71432=CARTESIAN_POINT ( 'NONE',  ( -18.40000000000000213, 70.35000000001187459, -90.37310748452433984 ) ) ;
#71485=CARTESIAN_POINT ( 'NONE',  ( -16.83794479845801817, 66.07364258066029095, -82.32666278030205831 ) ) ;
#71487=DIRECTION ( 'NONE',  ( 0.7071067811865463515, 0.7071067811865487940, 4.937700262164540154E-15 ) ) ;
#71646=CARTESIAN_POINT ( 'NONE',  ( -18.34374000495060386, 64.52683809664941350, -93.77310748452440237 ) ) ;
#71668=AXIS2_PLACEMENT_3D ( 'NONE', #50041, #166178, #27951 ) ;
#72159=CARTESIAN_POINT ( 'NONE',  ( -17.05016517656038744, 66.05000000000937632, -90.35040948852557108 ) ) ;
#72355=ORIENTED_EDGE ( 'NONE', *, *, #177166, .F. ) ;
#72779=CARTESIAN_POINT ( 'NONE',  ( -16.80469485234340610, 66.05784833687079072, -82.21314064059320970 ) ) ;
#72872=DIRECTION ( 'NONE',  ( 0.5932847527679310229, 0.8049926720990042694, 5.621233785078285907E-15 ) ) ;
#72919=CARTESIAN_POINT ( 'NONE',  ( 23.04999999999999716, 67.17743825834540417, -82.17310748452437963 ) ) ;
#73098=FACE_OUTER_BOUND ( 'NONE', #92255, .T. ) ;
#73135=DIRECTION ( 'NONE',  ( -1.000000000000000000, 0.000000000000000000, 0.000000000000000000 ) ) ;
#73343=FACE_OUTER_BOUND ( 'NONE', #33209, .T. ) ;
#73382=B_SPLINE_CURVE_WITH_KNOTS ( 'NONE', 3,
 ( #224274, #144726, #226846, #126466, #7816, #203443, #24831 ),
 .UNSPECIFIED., .F., .F.,
 ( 4, 3, 4 ),
 ( 3.469446951953614189E-18, 3.882884552234413058E-05, 5.798605692158429121E-05 ),
 .UNSPECIFIED. ) ;
#73623=CIRCLE ( 'NONE', #252453, 1.749999999999999778 ) ;
#73800=CARTESIAN_POINT ( 'NONE',  ( -16.78493832629887805, 66.05416425680772363, -90.35915846542016538 ) ) ;
#73961=AXIS2_PLACEMENT_3D ( 'NONE', #230913, #108382, #73135 ) ;
#74638=PLANE ( 'NONE',  #215384 ) ;
#74680=FACE_OUTER_BOUND ( 'NONE', #245735, .T. ) ;
#74769=VECTOR ( 'NONE', #174551, 1000.000000000000000 ) ;
#74789=ORIENTED_EDGE ( 'NONE', *, *, #213937, .F. ) ;
#74825=CARTESIAN_POINT ( 'NONE',  ( -23.25000000000000355, 70.35000000001187459, -90.37310748452433984 ) ) ;
#75001=CARTESIAN_POINT ( 'NONE',  ( 14.56326696814971200, 66.55335100938299320, -87.93394418860121675 ) ) ;
#75023=CARTESIAN_POINT ( 'NONE',  ( -16.93860193097148326, 66.00689223268254580, -82.12296911721753645 ) ) ;
#75086=CARTESIAN_POINT ( 'NONE',  ( -16.87683809663752399, 66.15000000001187175, -89.62074346632807931 ) ) ;
#75145=ORIENTED_EDGE ( 'NONE', *, *, #88142, .T. ) ;
#75257=DIRECTION ( 'NONE',  ( 0.000000000000000000, -1.000000000000000000, -6.982962677686266711E-15 ) ) ;
#75629=CYLINDRICAL_SURFACE ( 'NONE', #112259, 1.749999999999999778 ) ;
#75642=EDGE_CURVE ( 'NONE', #77215, #76792, #143750, .T. ) ;
#75687=EDGE_CURVE ( 'NONE', #83024, #200313, #166661, .T. ) ;
#75790=B_SPLINE_CURVE_WITH_KNOTS ( 'NONE', 3,
 ( #92302, #192703, #55706, #153623, #231840, #177016, #154882, #51877, #193997, #171888 ),
 .UNSPECIFIED., .F., .F.,
 ( 4, 3, 3, 4 ),
 ( 0.000000000000000000, 1.004626015991719593E-05, 1.831183478183680716E-05, 2.062343583996558100E-05 ),
 .UNSPECIFIED. ) ;
#75846=DIRECTION ( 'NONE',  ( 1.186688945009009831E-16, 1.000000000000000000, 6.982962677686266711E-15 ) ) ;
#75956=CIRCLE ( 'NONE', #242539, 0.09999999999999939493 ) ;
#76203=ORIENTED_EDGE ( 'NONE', *, *, #68258, .F. ) ;
#76265=CARTESIAN_POINT ( 'NONE',  ( -16.97683810757273193, 66.05000000001187743, -89.75953077206389707 ) ) ;
#76393=VERTEX_POINT ( 'NONE', #240966 ) ;
#76627=FACE_OUTER_BOUND ( 'NONE', #53380, .T. ) ;
#76690=ORIENTED_EDGE ( 'NONE', *, *, #93137, .F. ) ;
#76702=DIRECTION ( 'NONE',  ( 1.186688945009010077E-16, 1.000000000000000000, 6.982962677686266711E-15 ) ) ;
#76762=EDGE_CURVE ( 'NONE', #10328, #7257, #172757, .T. ) ;
#76792=VERTEX_POINT ( 'NONE', #43738 ) ;
#76801=EDGE_LOOP ( 'NONE', ( #240319, #217805, #133834, #182150, #55460, #188949, #176213, #29943, #61715, #8851, #215222, #15273 ) ) ;
#77123=FACE_OUTER_BOUND ( 'NONE', #248609, .T. ) ;
#77215=VERTEX_POINT ( 'NONE', #186483 ) ;
#77231=CARTESIAN_POINT ( 'NONE',  ( -16.90202395485798093, 66.03405545546124245, -90.42612120578500878 ) ) ;
#77332=DIRECTION ( 'NONE',  ( 0.000000000000000000, -1.000000000000000000, -6.982962677686266711E-15 ) ) ;
#77593=CARTESIAN_POINT ( 'NONE',  ( -16.85312841634287295, 66.08639382269167584, -90.12593435123184804 ) ) ;
#77679=VERTEX_POINT ( 'NONE', #176894 ) ;
#78050=DIRECTION ( 'NONE',  ( 1.000000000000000000, -1.186688945009010077E-16, -8.286604613020808509E-31 ) ) ;
#78069=ORIENTED_EDGE ( 'NONE', *, *, #43363, .F. ) ;
#78150=CARTESIAN_POINT ( 'NONE',  ( -16.81744102076749314, 66.05000000001187743, -90.37310748452438247 ) ) ;
#78217=CARTESIAN_POINT ( 'NONE',  ( -16.77683809663752257, 66.05000000001182059, -82.17310748452439384 ) ) ;
#78248=DIRECTION ( 'NONE',  ( 1.000000000000000000, -1.186688945009010077E-16, -8.286604613020808509E-31 ) ) ;
#78649=LINE ( 'NONE', #82485, #23576 ) ;
#78688=AXIS2_PLACEMENT_3D ( 'NONE', #224671, #184268, #66895 ) ;
#78795=CARTESIAN_POINT ( 'NONE',  ( -16.87683809663752399, 66.15000000001182912, -82.92547150272069700 ) ) ;
#78820=CARTESIAN_POINT ( 'NONE',  ( -16.87401514999235275, 66.05000000001187743, -90.30312547705619863 ) ) ;
#78950=VECTOR ( 'NONE', #95729, 1000.000000000000000 ) ;
#78997=ORIENTED_EDGE ( 'NONE', *, *, #27254, .T. ) ;
#79052=CARTESIAN_POINT ( 'NONE',  ( -13.11924609551135568, 66.56831044948773979, -84.74381745228834006 ) ) ;
#79213=UNCERTAINTY_MEASURE_WITH_UNIT (LENGTH_MEASURE( 1.000000000000000082E-05 ), #209015, 'distance_accuracy_value', 'NONE');
#79281=DIRECTION ( 'NONE',  ( -0.000000000000000000, -6.982962677686266711E-15, 1.000000000000000000 ) ) ;
#79405=CARTESIAN_POINT ( 'NONE',  ( -15.15766958671844300, 66.58946139148297050, -87.59041948738348538 ) ) ;
#79873=( NAMED_UNIT ( * ) SI_UNIT ( $, .STERADIAN. ) SOLID_ANGLE_UNIT ( ) );
#80117=VECTOR ( 'NONE', #117506, 1000.000000000000000 ) ;
#80183=ORIENTED_EDGE ( 'NONE', *, *, #143309, .F. ) ;
#80266=DIRECTION ( 'NONE',  ( -1.000000000000000000, 0.000000000000000000, -0.000000000000000000 ) ) ;
#80814=DIRECTION ( 'NONE',  ( 1.000000000000000000, 0.000000000000000000, 0.000000000000000000 ) ) ;
#81088=AXIS2_PLACEMENT_3D ( 'NONE', #81888, #203154, #162767 ) ;
#81105=CARTESIAN_POINT ( 'NONE',  ( 18.39999999999999503, 64.25000000001182343, -82.17310748452439384 ) ) ;
#81166=PRESENTATION_STYLE_ASSIGNMENT (( #100712 ) ) ;
#81413=DIRECTION ( 'NONE',  ( -1.000000000000000000, 0.000000000000000000, 0.000000000000000000 ) ) ;
#81650=VERTEX_POINT ( 'NONE', #187311 ) ;
#81888=CARTESIAN_POINT ( 'NONE',  ( 13.99999999999999822, 66.15000000001185754, -86.27310748452437394 ) ) ;
#81937=EDGE_CURVE ( 'NONE', #232261, #69456, #12913, .T. ) ;
#81940=VECTOR ( 'NONE', #24615, 1000.000000000000000 ) ;
#81974=CARTESIAN_POINT ( 'NONE',  ( 20.73486653747088226, 68.75000000001183764, -90.37310748452435405 ) ) ;
#82002=CIRCLE ( 'NONE', #102278, 1.500000000000001332 ) ;
#82485=CARTESIAN_POINT ( 'NONE',  ( -33.72168855820451938, 66.05000000001180638, -82.17310748452433700 ) ) ;
#82765=CARTESIAN_POINT ( 'NONE',  ( -18.34374000495060386, 64.52683809664941350, -93.77310748452440237 ) ) ;
#83024=VERTEX_POINT ( 'NONE', #55466 ) ;
#83058=ORIENTED_EDGE ( 'NONE', *, *, #184590, .T. ) ;
#83077=AXIS2_PLACEMENT_3D ( 'NONE', #157788, #138150, #133052 ) ;
#83162=ORIENTED_EDGE ( 'NONE', *, *, #92479, .F. ) ;
#83263=LINE ( 'NONE', #6312, #165564 ) ;
#83422=CIRCLE ( 'NONE', #137586, 0.5000000000000004441 ) ;
#83625=EDGE_CURVE ( 'NONE', #119515, #24606, #104577, .T. ) ;
#83739=DIRECTION ( 'NONE',  ( 0.5932847527679299127, 0.8049926720990051576, 4.984624513800587583E-15 ) ) ;
#83810=CARTESIAN_POINT ( 'NONE',  ( -16.92570016628983609, 66.04121104227196781, -82.14375815456340035 ) ) ;
#84110=CARTESIAN_POINT ( 'NONE',  ( -16.93302609847409457, 66.00331747920864700, -90.43671898916183238 ) ) ;
#84216=CIRCLE ( 'NONE', #200810, 0.1000000000000028644 ) ;
#84485=ORIENTED_EDGE ( 'NONE', *, *, #19883, .T. ) ;
#84491=CARTESIAN_POINT ( 'NONE',  ( -16.87036670365548474, 66.01058118071016168, -82.04354736722233099 ) ) ;
#85014=ORIENTED_EDGE ( 'NONE', *, *, #184590, .F. ) ;
#85061=CIRCLE ( 'NONE', #234952, 14.30833333333333890 ) ;
#85109=CARTESIAN_POINT ( 'NONE',  ( 18.54999999999999716, 67.25000000001185185, -93.77310748452437394 ) ) ;
#85333=EDGE_LOOP ( 'NONE', ( #233755, #136063, #243372, #102422 ) ) ;
#85743=CARTESIAN_POINT ( 'NONE',  ( -16.94333152882356330, 66.00965798855413880, -82.13107595342289358 ) ) ;
#85826=DIRECTION ( 'NONE',  ( 0.000000000000000000, -1.000000000000000000, -6.982962677686266711E-15 ) ) ;
#85965=B_SPLINE_CURVE_WITH_KNOTS ( 'NONE', 3,
 ( #104410, #163145, #242654, #183974, #45745, #165719, #66603, #125294, #226955, #246510 ),
 .UNSPECIFIED., .F., .F.,
 ( 4, 2, 2, 2, 4 ),
 ( 0.000000000000000000, 0.0003916577441626822214, 0.0005874866162440240368, 0.0006854010522846949987, 0.0007833154883253658522 ),
 .UNSPECIFIED. ) ;
#86502=EDGE_CURVE ( 'NONE', #217324, #146896, #46668, .T. ) ;
#86629=VERTEX_POINT ( 'NONE', #169243 ) ;
#86830=FACE_OUTER_BOUND ( 'NONE', #20324, .T. ) ;
#86970=CARTESIAN_POINT ( 'NONE',  ( -18.40000000000000213, 64.52683809664929981, -78.84905355133234650 ) ) ;
#87117=DIRECTION ( 'NONE',  ( 0.000000000000000000, -6.982962677686266711E-15, 1.000000000000000000 ) ) ;
#87469=DIRECTION ( 'NONE',  ( -1.020425574104004196E-15, -6.982962677686266711E-15, 1.000000000000000000 ) ) ;
#87489=B_SPLINE_CURVE_WITH_KNOTS ( 'NONE', 3,
 ( #146425, #47326, #208989, #172487, #13369, #34241, #51168, #227262, #171198, #249415, #212853, #48625, #30373, #70795, #193295, #229839, #12103, #147742, #89032, #129457, #112475, #32972, #232432, #113739, #168639, #189439, #248112, #52464, #128176, #14676 ),
 .UNSPECIFIED., .F., .F.,
 ( 4, 2, 2, 2, 2, 2, 2, 2, 2, 2, 2, 2, 2, 2, 4 ),
 ( 0.000000000000000000, 0.0003422764154113352953, 0.0006845528308226705907, 0.001026829246234005778, 0.001369105661645341181, 0.002053658492468005484, 0.002738211323290670220, 0.003080487738702004756, 0.003422764154113338859, 0.003765040569524673829, 0.004107316984936008365, 0.004449593400347343769, 0.004791869815758677438, 0.005134146231170012842, 0.005476422646581347378 ),
 .UNSPECIFIED. ) ;
#87499=EDGE_CURVE ( 'NONE', #41846, #26102, #130748, .T. ) ;
#87626=ORIENTED_EDGE ( 'NONE', *, *, #20164, .F. ) ;
#87786=CARTESIAN_POINT ( 'NONE',  ( -16.87998658237740912, 66.05000000001182059, -82.38674705226230799 ) ) ;
#87808=CARTESIAN_POINT ( 'NONE',  ( -16.80621392010908011, 66.05779742250405207, -90.33351551910763533 ) ) ;
#88078=FACE_OUTER_BOUND ( 'NONE', #215021, .T. ) ;
#88142=EDGE_CURVE ( 'NONE', #52520, #91770, #228917, .T. ) ;
#88417=ADVANCED_FACE ( 'NONE', ( #257393 ), #54756, .F. ) ;
#88603=EDGE_CURVE ( 'NONE', #247441, #64278, #82002, .T. ) ;
#88747=CARTESIAN_POINT ( 'NONE',  ( -16.27683809663751191, 66.65000000001191438, -93.77310748452441658 ) ) ;
#89032=CARTESIAN_POINT ( 'NONE',  ( 13.12229106158773639, 66.56936289831510578, -84.75484686646345267 ) ) ;
#89075=CARTESIAN_POINT ( 'NONE',  ( -16.86133551771148475, 66.05000000001182059, -82.22176404997772181 ) ) ;
#89252=VECTOR ( 'NONE', #12393, 1000.000000000000000 ) ;
#89308=ADVANCED_FACE ( 'NONE', ( #76627 ), #231882, .F. ) ;
#89514=B_SPLINE_CURVE_WITH_KNOTS ( 'NONE', 3,
 ( #192697, #252644, #91021, #231832, #125343, #71485, #152310, #104461, #32368, #72779, #203588, #24979, #250100, #164474 ),
 .UNSPECIFIED., .F., .F.,
 ( 4, 2, 2, 2, 2, 2, 4 ),
 ( 1.387778780781445676E-17, 0.0003823333598417443468, 0.0005735000397626304793, 0.0006690833797230903235, 0.0007168750497033217093, 0.0007407708846934326317, 0.0007646667196835435542 ),
 .UNSPECIFIED. ) ;
#89527=CARTESIAN_POINT ( 'NONE',  ( 21.72449340488910252, 65.71604372252076587, -93.77310748452438816 ) ) ;
#89587=ADVANCED_FACE ( 'NONE', ( #225101 ), #229912, .T. ) ;
#89796=ORIENTED_EDGE ( 'NONE', *, *, #15470, .F. ) ;
#89858=VERTEX_POINT ( 'NONE', #201088 ) ;
#89969=DIRECTION ( 'NONE',  ( -1.000000000000000000, 0.000000000000000000, -0.000000000000000000 ) ) ;
#90017=LINE ( 'NONE', #108316, #241608 ) ;
#90059=LINE ( 'NONE', #69246, #129931 ) ;
#90070=DIRECTION ( 'NONE',  ( -0.000000000000000000, -6.982962677686266711E-15, 1.000000000000000000 ) ) ;
#90344=CARTESIAN_POINT ( 'NONE',  ( -16.80939487329394666, 66.05000000001182059, -82.17310748452349856 ) ) ;
#90508=PLANE ( 'NONE',  #180541 ) ;
#90728=ORIENTED_EDGE ( 'NONE', *, *, #255105, .T. ) ;
#91021=CARTESIAN_POINT ( 'NONE',  ( -16.87372397896796272, 66.11940046337004162, -82.67238297448861317 ) ) ;
#91289=VERTEX_POINT ( 'NONE', #220712 ) ;
#91668=B_SPLINE_CURVE_WITH_KNOTS ( 'NONE', 3,
 ( #170289, #251045, #189813, #194960, #253609, #54131, #193661, #210651, #112835, #11173, #13734, #249780, #191115, #75023, #12470, #172859 ),
 .UNSPECIFIED., .F., .F.,
 ( 4, 3, 3, 3, 3, 4 ),
 ( 0.000000000000000000, 1.810570668009477602E-05, 2.740575833571357316E-05, 4.256816319435821725E-05, 5.213463471025588320E-05, 6.641585710718402133E-05 ),
 .UNSPECIFIED. ) ;
#91706=EDGE_CURVE ( 'NONE', #197810, #92572, #38889, .T. ) ;
#91707=ADVANCED_FACE ( 'NONE', ( #118423 ), #197934, .F. ) ;
#91708=CARTESIAN_POINT ( 'NONE',  ( -16.97092634996626970, 65.99911103366400766, -90.39296471822643753 ) ) ;
#91745=B_SPLINE_CURVE_WITH_KNOTS ( 'NONE', 3,
 ( #223662, #5897, #22942, #140268, #183276, #184541, #25494, #200271, #84110, #120761, #122015, #102412, #124595, #144121, #65891, #159879, #4617, #101107, #221100 ),
 .UNSPECIFIED., .F., .F.,
 ( 4, 3, 3, 3, 3, 3, 4 ),
 ( 0.0001624081864585828479, 0.0001685232196531679001, 0.0001764526673566893435, 0.0001916878551483146103, 0.0002009890782182573881, 0.0002238845907555200366, 0.0002283406619926344556 ),
 .UNSPECIFIED. ) ;
#91752=CARTESIAN_POINT ( 'NONE',  ( 20.99999999999999645, 66.25000000001188027, -90.37310748452436826 ) ) ;
#91770=VERTEX_POINT ( 'NONE', #63556 ) ;
#91915=ORIENTED_EDGE ( 'NONE', *, *, #126993, .F. ) ;
#92098=ORIENTED_EDGE ( 'NONE', *, *, #204543, .T. ) ;
#92255=EDGE_LOOP ( 'NONE', ( #126527, #24866, #52336 ) ) ;
#92302=CARTESIAN_POINT ( 'NONE',  ( -16.87331047859649757, 66.05000000001182059, -82.17310748452439384 ) ) ;
#92479=EDGE_CURVE ( 'NONE', #100605, #98906, #78649, .T. ) ;
#92543=ADVANCED_FACE ( 'NONE', ( #18691 ), #103346, .F. ) ;
#92572=VERTEX_POINT ( 'NONE', #201180 ) ;
#92579=CARTESIAN_POINT ( 'NONE',  ( -18.39999999999999858, 64.52683809664941350, -93.69716141771641560 ) ) ;
#92646=AXIS2_PLACEMENT_3D ( 'NONE', #20730, #2409, #138072 ) ;
#92689=ORIENTED_EDGE ( 'NONE', *, *, #93137, .T. ) ;
#92763=VECTOR ( 'NONE', #94740, 1000.000000000000000 ) ;
#92798=( BOUNDED_CURVE ( )  B_SPLINE_CURVE ( 3, ( #71646, #192870, #151176, #230715 ),
 .UNSPECIFIED., .F., .F. ) 
 B_SPLINE_CURVE_WITH_KNOTS ( ( 4, 4 ),
 ( 5.731445031868798168, 5.983100554402349225 ),
 .UNSPECIFIED. ) 
 CURVE ( )  GEOMETRIC_REPRESENTATION_ITEM ( )  RATIONAL_B_SPLINE_CURVE ( ( 1.000000000000000000, 0.9947294176030464508, 0.9947294176030464508, 1.000000000000000000 ) ) 
 REPRESENTATION_ITEM ( '' )  );
#92834=VERTEX_POINT ( 'NONE', #97674 ) ;
#92959=EDGE_CURVE ( 'NONE', #26113, #83024, #128830, .T. ) ;
#93137=EDGE_CURVE ( 'NONE', #205773, #249247, #250050, .T. ) ;
#93183=DIRECTION ( 'NONE',  ( -1.646408749285562691E-14, -1.000000000000000000, -6.982962677686266711E-15 ) ) ;
#93351=AXIS2_PLACEMENT_3D ( 'NONE', #200763, #241191, #2545 ) ;
#93438=VECTOR ( 'NONE', #226590, 1000.000000000000000 ) ;
#94015=ORIENTED_EDGE ( 'NONE', *, *, #46866, .F. ) ;
#94105=TOROIDAL_SURFACE ( 'NONE', #69203, 14.20833333333334103, 0.1000000000000000056 ) ;
#94229=ADVANCED_FACE ( 'NONE', ( #73098 ), #69232, .F. ) ;
#94234=CARTESIAN_POINT ( 'NONE',  ( -16.91256925476571382, 66.01426884188369115, -90.49074997352965966 ) ) ;
#94425=CARTESIAN_POINT ( 'NONE',  ( -33.72168855820451938, 66.05000000001186322, -90.37310748452443931 ) ) ;
#94463=PLANE ( 'NONE',  #45527 ) ;
#94520=CARTESIAN_POINT ( 'NONE',  ( 14.45204356427541548, 66.54933111084433506, -87.96756099431701159 ) ) ;
#94594=ORIENTED_EDGE ( 'NONE', *, *, #135287, .F. ) ;
#94605=CARTESIAN_POINT ( 'NONE',  ( -16.87372386987899020, 66.11939976637512473, -89.87383761265797943 ) ) ;
#94674=CARTESIAN_POINT ( 'NONE',  ( 17.74533788810830259, 65.18150020854109528, -92.70948480957680715 ) ) ;
#94719=AXIS2_PLACEMENT_3D ( 'NONE', #237351, #160405, #80814 ) ;
#94726=ADVANCED_FACE ( 'NONE', ( #1849 ), #194899, .F. ) ;
#94740=DIRECTION ( 'NONE',  ( -0.5932847527679310229, -0.8049926720990042694, -4.984624513800578906E-15 ) ) ;
#94752=ORIENTED_EDGE ( 'NONE', *, *, #81937, .T. ) ;
#94762=VECTOR ( 'NONE', #228224, 1000.000000000000000 ) ;
#95141=CARTESIAN_POINT ( 'NONE',  ( -12.25000000000000711, 66.65000000001188596, -86.50453852712175262 ) ) ;
#95168=EDGE_CURVE ( 'NONE', #121571, #69398, #56394, .T. ) ;
#95618=CARTESIAN_POINT ( 'NONE',  ( -15.75000000000000355, 66.15000000001185754, -86.27310748452437394 ) ) ;
#95623=LINE ( 'NONE', #57774, #161137 ) ;
#95729=DIRECTION ( 'NONE',  ( 0.000000000000000000, 6.982962677686266711E-15, -1.000000000000000000 ) ) ;
#95815=CARTESIAN_POINT ( 'NONE',  ( -16.97683809663752186, 66.05000000001187743, -89.62074346632789457 ) ) ;
#95954=CARTESIAN_POINT ( 'NONE',  ( 18.39999999999998082, 64.52683809664941350, -93.77310748452438816 ) ) ;
#96012=CARTESIAN_POINT ( 'NONE',  ( -23.25000000000000355, 64.25000000001182343, -82.17310748452439384 ) ) ;
#96348=ORIENTED_EDGE ( 'NONE', *, *, #7805, .T. ) ;
#96403=CARTESIAN_POINT ( 'NONE',  ( -15.75000000000000355, 66.65000000001185754, -86.27310748452437394 ) ) ;
#96428=DIRECTION ( 'NONE',  ( 1.186688945009010077E-16, 1.000000000000000000, 6.982962677686266711E-15 ) ) ;
#96572=VECTOR ( 'NONE', #198840, 1000.000000000000000 ) ;
#96614=ORIENTED_EDGE ( 'NONE', *, *, #30064, .T. ) ;
#96939=CARTESIAN_POINT ( 'NONE',  ( -16.92925196614874750, 66.02766820360174904, -90.40636263680760010 ) ) ;
#96946=DIRECTION ( 'NONE',  ( 1.000000000000000000, 0.000000000000000000, 0.000000000000000000 ) ) ;
#96986=ADVANCED_FACE ( 'NONE', ( #127448 ), #124883, .F. ) ;
#97121=CARTESIAN_POINT ( 'NONE',  ( -16.92507428761700439, 66.05000000001187743, -90.30971002490282729 ) ) ;
#97202=AXIS2_PLACEMENT_3D ( 'NONE', #225758, #45858, #241497 ) ;
#97623=DIRECTION ( 'NONE',  ( -0.000000000000000000, -6.982962677686266711E-15, 1.000000000000000000 ) ) ;
#97638=CARTESIAN_POINT ( 'NONE',  ( -17.01473183483380680, 66.05000000001182059, -82.27310748452441658 ) ) ;
#97674=CARTESIAN_POINT ( 'NONE',  ( 22.88900146558018989, 67.29609520889898988, -82.17310748452437963 ) ) ;
#97797=B_SPLINE_CURVE_WITH_KNOTS ( 'NONE', 3,
 ( #218071, #100677, #124147, #39494, #19911, #42044, #180259, #119007, #98110, #121597 ),
 .UNSPECIFIED., .F., .F.,
 ( 4, 3, 3, 4 ),
 ( 0.000000000000000000, 4.874959354401577961E-05, 9.785140065119720494E-05, 0.0001360444631935916505 ),
 .UNSPECIFIED. ) ;
#97801=PLANE ( 'NONE',  #94719 ) ;
#98110=CARTESIAN_POINT ( 'NONE',  ( -16.88495309932523014, 66.04537294153901428, -90.38855881071248177 ) ) ;
#98486=CARTESIAN_POINT ( 'NONE',  ( -18.40000000000000213, 64.52683809664929981, -78.77310748452438816 ) ) ;
#98683=CARTESIAN_POINT ( 'NONE',  ( 18.39999999999999503, 64.25000000001188027, -90.37310748452439668 ) ) ;
#98898=ORIENTED_EDGE ( 'NONE', *, *, #177166, .T. ) ;
#98906=VERTEX_POINT ( 'NONE', #108593 ) ;
#98907=DIRECTION ( 'NONE',  ( 1.000000000000000000, 0.000000000000000000, 0.000000000000000000 ) ) ;
#98923=DIRECTION ( 'NONE',  ( -1.000000000000000000, 7.492892343619937423E-30, -1.073024830501117725E-15 ) ) ;
#98978=CARTESIAN_POINT ( 'NONE',  ( -16.78055652883087134, 66.05322308388652175, -90.36231564693194684 ) ) ;
#99006=AXIS2_PLACEMENT_3D ( 'NONE', #18604, #137255, #38182 ) ;
#99567=LINE ( 'NONE', #116596, #241494 ) ;
#99587=CARTESIAN_POINT ( 'NONE',  ( -18.41431012584569160, 64.51252797080363166, -78.74987147142272192 ) ) ;
#99866=CARTESIAN_POINT ( 'NONE',  ( -17.29158576265543346, 65.63525233399396086, -91.60586572931654814 ) ) ;
#100126=FACE_OUTER_BOUND ( 'NONE', #110696, .T. ) ;
#100145=ORIENTED_EDGE ( 'NONE', *, *, #8314, .T. ) ;
#100167=ORIENTED_EDGE ( 'NONE', *, *, #29087, .F. ) ;
#100193=ORIENTED_EDGE ( 'NONE', *, *, #151310, .T. ) ;
#100259=EDGE_CURVE ( 'NONE', #54224, #10328, #90059, .T. ) ;
#100338=EDGE_LOOP ( 'NONE', ( #190025, #36728, #85014, #238536, #229105, #103119, #243728, #165728, #141614 ) ) ;
#100500=CARTESIAN_POINT ( 'NONE',  ( -23.25000000000000355, 64.25000000001190870, -93.77310748452438816 ) ) ;
#100593=DIRECTION ( 'NONE',  ( -1.000000000000000000, -1.652117596168391700E-15, -1.153667551319263085E-29 ) ) ;
#100605=VERTEX_POINT ( 'NONE', #179900 ) ;
#100677=CARTESIAN_POINT ( 'NONE',  ( -16.86578989773641979, 66.01519019875307492, -90.48777237114661887 ) ) ;
#100712=SURFACE_STYLE_USAGE ( .BOTH. , #203709 ) ;
#100806=CARTESIAN_POINT ( 'NONE',  ( -16.91256925476570672, 66.01426884188362010, -82.05546499551910244 ) ) ;
#100827=VERTEX_POINT ( 'NONE', #137534 ) ;
#100877=ORIENTED_EDGE ( 'NONE', *, *, #92959, .T. ) ;
#100883=CARTESIAN_POINT ( 'NONE',  ( -16.77683809663752257, 66.05416425680765258, -82.18705650362858250 ) ) ;
#101107=CARTESIAN_POINT ( 'NONE',  ( -16.94037747912386394, 65.98646061752553749, -90.47197652654890021 ) ) ;
#101189=ORIENTED_EDGE ( 'NONE', *, *, #126500, .F. ) ;
#101485=DIRECTION ( 'NONE',  ( -1.020425574104004196E-15, 6.982962677686266711E-15, -1.000000000000000000 ) ) ;
#101501=( BOUNDED_CURVE ( )  B_SPLINE_CURVE ( 3, ( #69865, #225037, #67269, #146787 ),
 .UNSPECIFIED., .F., .T. ) 
 B_SPLINE_CURVE_WITH_KNOTS ( ( 4, 4 ),
 ( 1.570796326794892339, 3.141592653589784678 ),
 .UNSPECIFIED. ) 
 CURVE ( )  GEOMETRIC_REPRESENTATION_ITEM ( )  RATIONAL_B_SPLINE_CURVE ( ( 1.000000000000000000, 0.8047378541243659367, 0.8047378541243659367, 1.000000000000000000 ) ) 
 REPRESENTATION_ITEM ( '' )  );
#101646=FACE_OUTER_BOUND ( 'NONE', #100338, .T. ) ;
#101961=PLANE ( 'NONE',  #203401 ) ;
#101999=SURFACE_STYLE_FILL_AREA ( #141170 ) ;
#102056=DIRECTION ( 'NONE',  ( 1.000000000000000000, 0.000000000000000000, 0.000000000000000000 ) ) ;
#102104=CARTESIAN_POINT ( 'NONE',  ( -16.86445178670700784, 66.03778837089569720, -82.13233004640675006 ) ) ;
#102145=ORIENTED_EDGE ( 'NONE', *, *, #60651, .F. ) ;
#102278=AXIS2_PLACEMENT_3D ( 'NONE', #150365, #135900, #194646 ) ;
#102285=LINE ( 'NONE', #200147, #247411 ) ;
#102374=CARTESIAN_POINT ( 'NONE',  ( 16.27683809663750125, 66.65000000001191438, -93.77310748452437394 ) ) ;
#102412=CARTESIAN_POINT ( 'NONE',  ( -16.93230518875208190, 65.99924963859201910, -90.44732913642287997 ) ) ;
#102422=ORIENTED_EDGE ( 'NONE', *, *, #59591, .F. ) ;
#102458=CARTESIAN_POINT ( 'NONE',  ( -15.06720934482788188, 66.58230930894875144, -84.88150678775981817 ) ) ;
#102642=EDGE_LOOP ( 'NONE', ( #196755, #94015, #158263, #14328, #228373 ) ) ;
#102932=MECHANICAL_DESIGN_GEOMETRIC_PRESENTATION_REPRESENTATION('',(#148764),#219459);
#103119=ORIENTED_EDGE ( 'NONE', *, *, #86502, .F. ) ;
#103297=( NAMED_UNIT ( * ) PLANE_ANGLE_UNIT ( ) SI_UNIT ( $, .RADIAN. ) );
#103346=CYLINDRICAL_SURFACE ( 'NONE', #2670, 1.749999999999999778 ) ;
#103392=CARTESIAN_POINT ( 'NONE',  ( -16.89318236219975944, 66.04846474213667307, -82.16797785241854513 ) ) ;
#103536=ORIENTED_EDGE ( 'NONE', *, *, #249144, .F. ) ;
#103549=CARTESIAN_POINT ( 'NONE',  ( 15.48841904831874849, 67.43841904833058720, -82.17310748452437963 ) ) ;
#103638=VERTEX_POINT ( 'NONE', #82765 ) ;
#103832=EDGE_CURVE ( 'NONE', #41846, #48436, #164915, .T. ) ;
#103957=DIRECTION ( 'NONE',  ( 1.186688945009009831E-16, 1.000000000000000000, 6.982962677686266711E-15 ) ) ;
#104046=ORIENTED_EDGE ( 'NONE', *, *, #216038, .T. ) ;
#104086=B_SPLINE_CURVE_WITH_KNOTS ( 'NONE', 3,
 ( #100883, #222130, #160924, #240447, #61811, #108635, #207758, #52495, #90344, #149069 ),
 .UNSPECIFIED., .F., .F.,
 ( 4, 3, 3, 4 ),
 ( -2.000561356209491534E-06, 0.000000000000000000, 1.787822682428948123E-05, 4.206475347090082037E-05 ),
 .UNSPECIFIED. ) ;
#104094=CARTESIAN_POINT ( 'NONE',  ( 20.27550659511088682, 66.78395627750303731, -93.77310748452437394 ) ) ;
#104309=CIRCLE ( 'NONE', #233534, 0.09999999999999516220 ) ;
#104340=EDGE_CURVE ( 'NONE', #121302, #77215, #39918, .T. ) ;
#104410=CARTESIAN_POINT ( 'NONE',  ( -16.97683809663752186, 66.05000000001187743, -89.62074346632789457 ) ) ;
#104418=ORIENTED_EDGE ( 'NONE', *, *, #153652, .T. ) ;
#104461=CARTESIAN_POINT ( 'NONE',  ( -16.81931177881022066, 66.06300394050791169, -82.24988960590717113 ) ) ;
#104515=FACE_OUTER_BOUND ( 'NONE', #166382, .T. ) ;
#104577=LINE ( 'NONE', #8091, #233157 ) ;
#104765=DIRECTION ( 'NONE',  ( 1.000000000000000000, 0.000000000000000000, 0.000000000000000000 ) ) ;
#105251=AXIS2_PLACEMENT_3D ( 'NONE', #89527, #230327, #133797 ) ;
#105465=CARTESIAN_POINT ( 'NONE',  ( -18.40000000000000213, 70.35000000001187459, -90.37310748452433984 ) ) ;
#105501=CARTESIAN_POINT ( 'NONE',  ( -20.65000000000000568, 68.75000000001182343, -82.17310748452436542 ) ) ;
#105504=ORIENTED_EDGE ( 'NONE', *, *, #115526, .T. ) ;
#105573=DIRECTION ( 'NONE',  ( 0.000000000000000000, -6.982962677686266711E-15, 1.000000000000000000 ) ) ;
#105758=AXIS2_PLACEMENT_3D ( 'NONE', #256928, #177482, #105573 ) ;
#105795=EDGE_LOOP ( 'NONE', ( #31467, #141539 ) ) ;
#105802=PLANE ( 'NONE',  #97202 ) ;
#105884=CARTESIAN_POINT ( 'NONE',  ( 21.72449340488910607, 65.71604372252069481, -82.17310748452439384 ) ) ;
#106359=CARTESIAN_POINT ( 'NONE',  ( -18.40000000000000213, 64.58541674041201475, -82.17310748452442226 ) ) ;
#106507=EDGE_CURVE ( 'NONE', #92572, #26497, #33476, .T. ) ;
#106541=CARTESIAN_POINT ( 'NONE',  ( -17.29158576265543346, 65.63525233399388981, -80.94034923973221396 ) ) ;
#106984=CARTESIAN_POINT ( 'NONE',  ( -16.86578989773640913, 66.01519019875300387, -82.05844259790215744 ) ) ;
#107190=CARTESIAN_POINT ( 'NONE',  ( 20.99999999999999645, 66.25000000001182343, -82.17310748452439384 ) ) ;
#107211=EDGE_CURVE ( 'NONE', #117904, #144564, #83422, .T. ) ;
#107362=CARTESIAN_POINT ( 'NONE',  ( -16.88783316861808359, 66.05000000001182059, -82.27537152650414498 ) ) ;
#107372=VECTOR ( 'NONE', #215214, 1000.000000000000000 ) ;
#107533=DIRECTION ( 'NONE',  ( -0.000000000000000000, -6.982962677686266711E-15, 1.000000000000000000 ) ) ;
#107743=CARTESIAN_POINT ( 'NONE',  ( -17.11825945287481687, 66.05000000001182059, -82.27310748452438816 ) ) ;
#108082=DIRECTION ( 'NONE',  ( 0.000000000000000000, 1.000000000000000000, 6.982962677686266711E-15 ) ) ;
#108275=FACE_OUTER_BOUND ( 'NONE', #19211, .T. ) ;
#108316=CARTESIAN_POINT ( 'NONE',  ( 23.24999999999999645, 64.25000000001190870, -93.77310748452438816 ) ) ;
#108322=DIRECTION ( 'NONE',  ( 0.000000000000000000, 0.000000000000000000, 1.000000000000000000 ) ) ;
#108382=DIRECTION ( 'NONE',  ( -0.000000000000000000, -6.982962677686266711E-15, 1.000000000000000000 ) ) ;
#108593=CARTESIAN_POINT ( 'NONE',  ( 18.54999999999999716, 66.05000000001180638, -82.17310748452433700 ) ) ;
#108635=CARTESIAN_POINT ( 'NONE',  ( -16.78805706634180339, 66.05174750694062880, -82.17895427649251872 ) ) ;
#108667=LINE ( 'NONE', #192076, #65160 ) ;
#109149=LINE ( 'NONE', #128740, #151320 ) ;
#109849=CARTESIAN_POINT ( 'NONE',  ( -17.78241384941283343, 65.14442424720841984, -92.77406981203996850 ) ) ;
#109850=CARTESIAN_POINT ( 'NONE',  ( 18.39999999999999503, 70.35000000001187459, -90.37310748452433984 ) ) ;
#109870=CARTESIAN_POINT ( 'NONE',  ( 22.88900146558018989, 67.29609520889906094, -93.77310748452437394 ) ) ;
#109897=( NAMED_UNIT ( * ) SI_UNIT ( $, .STERADIAN. ) SOLID_ANGLE_UNIT ( ) );
#109921=CARTESIAN_POINT ( 'NONE',  ( -16.94226253665225457, 66.05000000001183480, -82.46984208014016815 ) ) ;
#109925=AXIS2_PLACEMENT_3D ( 'NONE', #219028, #61253, #45540 ) ;
#109955=LINE ( 'NONE', #14748, #246216 ) ;
#110238=CARTESIAN_POINT ( 'NONE',  ( 15.39793903038207823, 66.61031399435617573, -87.35026397817307497 ) ) ;
#110317=DIRECTION ( 'NONE',  ( 1.000000000000000000, -1.646408749285562060E-14, -1.073024830501232702E-15 ) ) ;
#110354=ORIENTED_EDGE ( 'NONE', *, *, #59423, .F. ) ;
#110380=CIRCLE ( 'NONE', #210360, 0.9000000000000014655 ) ;
#110392=EDGE_LOOP ( 'NONE', ( #187517, #118106, #207609 ) ) ;
#110618=CARTESIAN_POINT ( 'NONE',  ( 20.99999999999999645, 66.25000000001188027, -90.37310748452436826 ) ) ;
#110696=EDGE_LOOP ( 'NONE', ( #189458, #3612, #153813, #157749, #63295 ) ) ;
#110820=VERTEX_POINT ( 'NONE', #48290 ) ;
#110824=CARTESIAN_POINT ( 'NONE',  ( -18.40000000000000213, 64.25000000001182343, -82.17310748452439384 ) ) ;
#111067=DIRECTION ( 'NONE',  ( 0.000000000000000000, -1.000000000000000000, -6.982962677686266711E-15 ) ) ;
#111151=CARTESIAN_POINT ( 'NONE',  ( -18.37013991200266005, 64.50025238379991777, -93.81613049504150581 ) ) ;
#111219=CARTESIAN_POINT ( 'NONE',  ( -16.97683809663752186, 66.05000000001183480, -82.92547150272069700 ) ) ;
#111508=CIRCLE ( 'NONE', #194915, 1.749999999999999778 ) ;
#111522=CARTESIAN_POINT ( 'NONE',  ( -18.40000000000000213, 64.52683809664931402, -82.07310748452439952 ) ) ;
#111590=EDGE_CURVE ( 'NONE', #236175, #232261, #211820, .T. ) ;
#111618=VERTEX_POINT ( 'NONE', #84491 ) ;
#111772=CARTESIAN_POINT ( 'NONE',  ( -16.90128866880176162, 66.04620422280885350, -82.16043130113574477 ) ) ;
#111991=AXIS2_PLACEMENT_3D ( 'NONE', #169570, #89969, #203516 ) ;
#112195=CARTESIAN_POINT ( 'NONE',  ( 23.24999999999999645, 70.35000000001187459, -90.37310748452433984 ) ) ;
#112259=AXIS2_PLACEMENT_3D ( 'NONE', #16927, #96428, #155178 ) ;
#112475=CARTESIAN_POINT ( 'NONE',  ( 12.84435279558020149, 66.58929125296475604, -84.95389907868030832 ) ) ;
#112533=FACE_OUTER_BOUND ( 'NONE', #178074, .T. ) ;
#112689=ORIENTED_EDGE ( 'NONE', *, *, #243343, .F. ) ;
#112835=CARTESIAN_POINT ( 'NONE',  ( -16.93234230245721861, 66.00189262946472013, -82.10541720285813483 ) ) ;
#113243=FACE_OUTER_BOUND ( 'NONE', #203500, .T. ) ;
#113739=CARTESIAN_POINT ( 'NONE',  ( 12.48201962039795809, 66.62334006147830223, -85.39491493630707453 ) ) ;
#113774=EDGE_CURVE ( 'NONE', #52520, #257124, #170641, .T. ) ;
#114014=PRODUCT_DEFINITION_SHAPE ( 'NONE', 'NONE',  #132936 ) ;
#114177=CARTESIAN_POINT ( 'NONE',  ( -16.85939591225058720, 66.09477352162400621, -90.06303923805535305 ) ) ;
#114569=ORIENTED_EDGE ( 'NONE', *, *, #141546, .T. ) ;
#114593=DIRECTION ( 'NONE',  ( 1.000000000000000000, 0.000000000000000000, 0.000000000000000000 ) ) ;
#114669=ORIENTED_EDGE ( 'NONE', *, *, #180172, .T. ) ;
#114703=CARTESIAN_POINT ( 'NONE',  ( -13.88555196119803270, 66.54256847116292306, -88.02319054662470421 ) ) ;
#114743=EDGE_LOOP ( 'NONE', ( #242753, #212102, #59035, #124079 ) ) ;
#114808=ORIENTED_EDGE ( 'NONE', *, *, #249144, .T. ) ;
#114969=CARTESIAN_POINT ( 'NONE',  ( -14.00000000000000178, 66.15000000001185754, -86.27310748452437394 ) ) ;
#114999=EDGE_CURVE ( 'NONE', #92834, #89858, #226288, .T. ) ;
#115046=STYLED_ITEM ( 'NONE', ( #66932 ), #14150 ) ;
#115081=DIRECTION ( 'NONE',  ( -0.000000000000000000, -6.982962677686266711E-15, 1.000000000000000000 ) ) ;
#115128=VECTOR ( 'NONE', #80266, 1000.000000000000000 ) ;
#115225=ADVANCED_FACE ( 'NONE', ( #10986 ), #90508, .F. ) ;
#115265=CARTESIAN_POINT ( 'NONE',  ( -14.00000000000000178, 66.15000000001185754, -86.27310748452437394 ) ) ;
#115370=ORIENTED_EDGE ( 'NONE', *, *, #256860, .T. ) ;
#115431=ORIENTED_EDGE ( 'NONE', *, *, #118304, .F. ) ;
#115437=CARTESIAN_POINT ( 'NONE',  ( -17.11825945287482753, 66.05000000001187743, -90.27310748452438816 ) ) ;
#115526=EDGE_CURVE ( 'NONE', #201406, #136022, #250569, .T. ) ;
#115847=DIRECTION ( 'NONE',  ( -1.000000000000000000, -1.652117596168391700E-15, -1.153667551319263085E-29 ) ) ;
#116228=EDGE_CURVE ( 'NONE', #209659, #86629, #109149, .T. ) ;
#116239=CARTESIAN_POINT ( 'NONE',  ( 20.04999999999999716, 67.25000000001178080, -82.17310748452437963 ) ) ;
#116596=CARTESIAN_POINT ( 'NONE',  ( 20.27550659511088682, 66.78395627750300889, -90.37310748452436826 ) ) ;
#116728=CARTESIAN_POINT ( 'NONE',  ( -17.01473183483381391, 66.05000000001187743, -90.27310748452437394 ) ) ;
#116739=CARTESIAN_POINT ( 'NONE',  ( 20.09999999999999787, 66.25000000001185185, -82.17310748452439384 ) ) ;
#116820=DIRECTION ( 'NONE',  ( 0.000000000000000000, 6.982962677686266711E-15, -1.000000000000000000 ) ) ;
#117119=DIRECTION ( 'NONE',  ( 0.000000000000000000, -6.982962677686266711E-15, 1.000000000000000000 ) ) ;
#117236=ORIENTED_EDGE ( 'NONE', *, *, #127109, .F. ) ;
#117278=CARTESIAN_POINT ( 'NONE',  ( -14.11697426661281085, 66.54258905524443435, -88.02302351073434750 ) ) ;
#117506=DIRECTION ( 'NONE',  ( -0.000000000000000000, -6.982962677686266711E-15, 1.000000000000000000 ) ) ;
#117527=EDGE_LOOP ( 'NONE', ( #129456, #173868, #204773, #170675 ) ) ;
#117593=DIRECTION ( 'NONE',  ( -0.000000000000000000, -6.982962677686266711E-15, 1.000000000000000000 ) ) ;
#117638=ORIENTED_EDGE ( 'NONE', *, *, #59960, .F. ) ;
#117836=ORIENTED_EDGE ( 'NONE', *, *, #92479, .T. ) ;
#117843=EDGE_CURVE ( 'NONE', #51021, #257124, #236845, .T. ) ;
#117904=VERTEX_POINT ( 'NONE', #184575 ) ;
#118020=CARTESIAN_POINT ( 'NONE',  ( 18.39999999999999503, 64.52683809664938508, -90.37310748452438247 ) ) ;
#118106=ORIENTED_EDGE ( 'NONE', *, *, #30170, .T. ) ;
#118235=VECTOR ( 'NONE', #61033, 999.9999999999998863 ) ;
#118304=EDGE_CURVE ( 'NONE', #69522, #34828, #219979, .T. ) ;
#118408=ORIENTED_EDGE ( 'NONE', *, *, #134569, .T. ) ;
#118423=FACE_OUTER_BOUND ( 'NONE', #45960, .T. ) ;
#118529=EDGE_CURVE ( 'NONE', #236196, #253194, #18767, .T. ) ;
#118590=EDGE_CURVE ( 'NONE', #26113, #56902, #99567, .T. ) ;
#118876=AXIS2_PLACEMENT_3D ( 'NONE', #85109, #25198, #3025 ) ;
#119007=CARTESIAN_POINT ( 'NONE',  ( -16.87845715379269507, 66.04214188611484815, -90.39930683346548790 ) ) ;
#119314=LINE ( 'NONE', #39805, #96572 ) ;
#119376=ORIENTED_EDGE ( 'NONE', *, *, #237414, .F. ) ;
#119409=DIRECTION ( 'NONE',  ( 0.000000000000000000, -1.000000000000000000, -6.982962677686266711E-15 ) ) ;
#119506=CARTESIAN_POINT ( 'NONE',  ( -14.22969084473441193, 66.54399267394249762, -84.53447399037760590 ) ) ;
#119515=VERTEX_POINT ( 'NONE', #167994 ) ;
#119781=CARTESIAN_POINT ( 'NONE',  ( 21.13736287352038445, 67.95335762362786625, -90.37310748452435405 ) ) ;
#119846=CARTESIAN_POINT ( 'NONE',  ( -16.89060415895971090, 66.04877923720965782, -90.37718726025393323 ) ) ;
#119990=ORIENTED_EDGE ( 'NONE', *, *, #54571, .F. ) ;
#120036=DIRECTION ( 'NONE',  ( -0.000000000000000000, -6.982962677686266711E-15, 1.000000000000000000 ) ) ;
#120402=CARTESIAN_POINT ( 'NONE',  ( -14.00000000000000178, 66.15000000001185754, -86.27310748452437394 ) ) ;
#120453=CARTESIAN_POINT ( 'NONE',  ( -16.89797118371545182, 66.02361927736747305, -82.08581411696629004 ) ) ;
#120499=CARTESIAN_POINT ( 'NONE',  ( -18.44085059012131822, 64.48598750652799083, -78.78280216540285608 ) ) ;
#120761=CARTESIAN_POINT ( 'NONE',  ( -16.93255653858138388, 66.00154854603471222, -90.44146411653470352 ) ) ;
#120770=ORIENTED_EDGE ( 'NONE', *, *, #176310, .T. ) ;
#120972=AXIS2_PLACEMENT_3D ( 'NONE', #63195, #3221, #162337 ) ;
#121302=VERTEX_POINT ( 'NONE', #21473 ) ;
#121409=ORIENTED_EDGE ( 'NONE', *, *, #30170, .F. ) ;
#121571=VERTEX_POINT ( 'NONE', #81105 ) ;
#121597=CARTESIAN_POINT ( 'NONE',  ( -16.89268316805466341, 66.04827818676967865, -90.37885996306994230 ) ) ;
#121919=PLANE ( 'NONE',  #120972 ) ;
#122015=CARTESIAN_POINT ( 'NONE',  ( -16.93226657140833069, 66.00045617728744674, -90.44439437355075029 ) ) ;
#122066=CARTESIAN_POINT ( 'NONE',  ( -15.69373346032659455, 66.64320997496594146, -85.81828097591048277 ) ) ;
#122469=VECTOR ( 'NONE', #154451, 1000.000000000000000 ) ;
#122754=VECTOR ( 'NONE', #79281, 1000.000000000000000 ) ;
#122959=LINE ( 'NONE', #163367, #147163 ) ;
#123006=PLANE ( 'NONE',  #118876 ) ;
#123094=CARTESIAN_POINT ( 'NONE',  ( -33.72168855820452649, 52.34166666667851331, -86.27310748452447342 ) ) ;
#123244=EDGE_CURVE ( 'NONE', #110820, #92834, #47201, .T. ) ;
#123393=CARTESIAN_POINT ( 'NONE',  ( -23.25000000000000355, 66.05000000001190585, -93.77310748452438816 ) ) ;
#123552=CARTESIAN_POINT ( 'NONE',  ( -14.00000000000000178, 66.15000000001185754, -86.27310748452437394 ) ) ;
#123599=CARTESIAN_POINT ( 'NONE',  ( -15.55912972643741199, 67.50912972644930221, -90.47310748452437679 ) ) ;
#123603=ADVANCED_FACE ( 'NONE', ( #3944 ), #5197, .F. ) ;
#124007=CARTESIAN_POINT ( 'NONE',  ( -16.89268316805465986, 66.04827818676963602, -82.16735500597883401 ) ) ;
#124079=ORIENTED_EDGE ( 'NONE', *, *, #104340, .T. ) ;
#124147=CARTESIAN_POINT ( 'NONE',  ( -16.86337532320261801, 66.02003279578751460, -90.47203195350718374 ) ) ;
#124379=CARTESIAN_POINT ( 'NONE',  ( -16.77180007708460963, 66.05000000001182059, -82.15872160347920783 ) ) ;
#124595=CARTESIAN_POINT ( 'NONE',  ( -16.93262454970420094, 65.99797953208150147, -90.45018371076169217 ) ) ;
#124700=DIRECTION ( 'NONE',  ( -1.020425574104004196E-15, 6.982962677686266711E-15, -1.000000000000000000 ) ) ;
#124707=DIRECTION ( 'NONE',  ( 0.000000000000000000, -6.789366196018718420E-15, 1.000000000000000000 ) ) ;
#124746=DIRECTION ( 'NONE',  ( 0.000000000000000000, -1.000000000000000000, -6.837150591533219968E-15 ) ) ;
#124883=CYLINDRICAL_SURFACE ( 'NONE', #233473, 0.1000000000000038219 ) ;
#124909=AXIS2_PLACEMENT_3D ( 'NONE', #218567, #75257, #233044 ) ;
#125149=EDGE_LOOP ( 'NONE', ( #151222, #117236, #78069, #121409, #28005 ) ) ;
#125202=SHAPE_REPRESENTATION ( 'Snap Open Cable Crossbars 14', ( #2425 ), #156768 ) ;
#125294=CARTESIAN_POINT ( 'NONE',  ( -16.86132326855785735, 66.05000000001189164, -90.32447169985607616 ) ) ;
#125332=ORIENTED_EDGE ( 'NONE', *, *, #142115, .F. ) ;
#125343=CARTESIAN_POINT ( 'NONE',  ( -16.85312964099708566, 66.08639531794410971, -82.42029177809392593 ) ) ;
#125483=DIRECTION ( 'NONE',  ( 1.073024830501117725E-15, -6.982962677686266711E-15, 1.000000000000000000 ) ) ;
#125554=CARTESIAN_POINT ( 'NONE',  ( -21.64999999999999858, 66.65000000001182912, -82.17310748452437963 ) ) ;
#125605=DIRECTION ( 'NONE',  ( -0.000000000000000000, -6.982962677686266711E-15, 1.000000000000000000 ) ) ;
#125611=( BOUNDED_CURVE ( )  B_SPLINE_CURVE ( 3, ( #58932, #62818, #23729, #158116 ),
 .UNSPECIFIED., .F., .F. ) 
 B_SPLINE_CURVE_WITH_KNOTS ( ( 4, 4 ),
 ( 3.432212674861196522, 3.693332928900581624 ),
 .UNSPECIFIED. ) 
 CURVE ( )  GEOMETRIC_REPRESENTATION_ITEM ( )  RATIONAL_B_SPLINE_CURVE ( ( 1.000000000000000000, 0.9943260843901261525, 0.9943260843901261525, 1.000000000000000000 ) ) 
 REPRESENTATION_ITEM ( '' )  );
#125869=VECTOR ( 'NONE', #114593, 1000.000000000000000 ) ;
#125970=VECTOR ( 'NONE', #111067, 1000.000000000000000 ) ;
#126022=ADVANCED_FACE ( 'NONE', ( #239242 ), #4467, .T. ) ;
#126080=CARTESIAN_POINT ( 'NONE',  ( -16.89268316805466341, 66.04827818676967865, -90.37885996306994230 ) ) ;
#126466=CARTESIAN_POINT ( 'NONE',  ( -18.38204789744325396, 64.52049896284670183, -78.77310748452438816 ) ) ;
#126500=EDGE_CURVE ( 'NONE', #98906, #153515, #174857, .T. ) ;
#126527=ORIENTED_EDGE ( 'NONE', *, *, #194625, .T. ) ;
#126683=ADVANCED_FACE ( 'NONE', ( #101646 ), #97801, .F. ) ;
#126938=CARTESIAN_POINT ( 'NONE',  ( -16.84981964351502270, 66.08268176591278120, -82.39270909854334946 ) ) ;
#126993=EDGE_CURVE ( 'NONE', #64278, #153515, #211058, .T. ) ;
#127109=EDGE_CURVE ( 'NONE', #111618, #76393, #69985, .T. ) ;
#127312=CARTESIAN_POINT ( 'NONE',  ( -16.93388492042257809, 66.01145817749589639, -82.12256236133821119 ) ) ;
#127324=CIRCLE ( 'NONE', #14915, 0.5000000000000004441 ) ;
#127448=FACE_OUTER_BOUND ( 'NONE', #225241, .T. ) ;
#127777=ORIENTED_EDGE ( 'NONE', *, *, #151310, .F. ) ;
#128054=DIRECTION ( 'NONE',  ( 1.000000000000000000, -1.541976423090492636E-14, 0.000000000000000000 ) ) ;
#128107=ORIENTED_EDGE ( 'NONE', *, *, #91706, .F. ) ;
#128114=ORIENTED_EDGE ( 'NONE', *, *, #216524, .F. ) ;
#128176=CARTESIAN_POINT ( 'NONE',  ( 12.25000000000000000, 66.65000000001185754, -86.15883987690831702 ) ) ;
#128227=CARTESIAN_POINT ( 'NONE',  ( -16.80891096016330621, 66.05000000001182059, -82.15544467725624145 ) ) ;
#128271=CARTESIAN_POINT ( 'NONE',  ( -16.91049119928363353, 66.05000000001190585, -90.40482787771522055 ) ) ;
#128355=VECTOR ( 'NONE', #135668, 1000.000000000000000 ) ;
#128740=CARTESIAN_POINT ( 'NONE',  ( 18.39999999999999503, 70.35000000001187459, -90.37310748452433984 ) ) ;
#128776=ORIENTED_EDGE ( 'NONE', *, *, #135923, .T. ) ;
#128803=CARTESIAN_POINT ( 'NONE',  ( -18.40000000000000213, 70.35000000001181775, -82.17310748452435121 ) ) ;
#128822=ORIENTED_EDGE ( 'NONE', *, *, #52061, .T. ) ;
#128830=LINE ( 'NONE', #104094, #81940 ) ;
#128929=FACE_OUTER_BOUND ( 'NONE', #76801, .T. ) ;
#129267=DIRECTION ( 'NONE',  ( -1.000000000000000000, 0.000000000000000000, -0.000000000000000000 ) ) ;
#129456=ORIENTED_EDGE ( 'NONE', *, *, #162695, .F. ) ;
#129457=CARTESIAN_POINT ( 'NONE',  ( 12.93279065517212345, 66.58230930894873723, -84.88150678775981817 ) ) ;
#129510=CARTESIAN_POINT ( 'NONE',  ( -16.84793658983463516, 66.05000000001182059, -82.25675416233410431 ) ) ;
#129555=CARTESIAN_POINT ( 'NONE',  ( -17.11825945287482753, 66.05000000001189164, -90.37310748452436826 ) ) ;
#129611=AXIS2_PLACEMENT_3D ( 'NONE', #38915, #136703, #54605 ) ;
#129800=DIRECTION ( 'NONE',  ( -0.000000000000000000, -6.982962677686266711E-15, 1.000000000000000000 ) ) ;
#129804=DIRECTION ( 'NONE',  ( 0.000000000000000000, 1.000000000000000000, 6.982962677686266711E-15 ) ) ;
#129805=CARTESIAN_POINT ( 'NONE',  ( 12.47034474403011828, 66.62446189796384033, -87.15323160353354126 ) ) ;
#129891=VECTOR ( 'NONE', #250123, 1000.000000000000000 ) ;
#129931=VECTOR ( 'NONE', #27574, 1000.000000000000000 ) ;
#129959=EDGE_CURVE ( 'NONE', #139023, #205773, #132276, .T. ) ;
#130057=CIRCLE ( 'NONE', #142528, 0.1000000000000028644 ) ;
#130488=CARTESIAN_POINT ( 'NONE',  ( 21.13736287352038445, 67.95335762362789467, -93.77310748452437394 ) ) ;
#130510=ADVANCED_FACE ( 'NONE', ( #108275 ), #7901, .F. ) ;
#130748=LINE ( 'NONE', #192033, #35270 ) ;
#130791=DIRECTION ( 'NONE',  ( -0.000000000000000000, -6.982962677686266711E-15, 1.000000000000000000 ) ) ;
#131673=CARTESIAN_POINT ( 'NONE',  ( -18.40000000000000213, 70.35000000001180354, -78.77310748452434552 ) ) ;
#131704=ORIENTED_EDGE ( 'NONE', *, *, #129959, .F. ) ;
#131806=CARTESIAN_POINT ( 'NONE',  ( -18.40000000000000213, 64.52683809664982562, -78.82293673299012937 ) ) ;
#132276=LINE ( 'NONE', #17465, #232620 ) ;
#132303=VECTOR ( 'NONE', #119409, 1000.000000000000000 ) ;
#132756=CARTESIAN_POINT ( 'NONE',  ( 12.25000000000000000, 66.65000000001185754, -86.27310748452437394 ) ) ;
#132773=DIRECTION ( 'NONE',  ( -1.000000000000000000, 4.625929269271478222E-14, 0.000000000000000000 ) ) ;
#132936=PRODUCT_DEFINITION ( 'UNKNOWN', '', #169630, #42672 ) ;
#133052=DIRECTION ( 'NONE',  ( 0.000000000000000000, 1.000000000000000000, 0.000000000000000000 ) ) ;
#133250=ORIENTED_EDGE ( 'NONE', *, *, #214199, .T. ) ;
#133298=EDGE_CURVE ( 'NONE', #205408, #91770, #58388, .T. ) ;
#133660=CARTESIAN_POINT ( 'NONE',  ( 13.43443725621852636, 66.55344247693932402, -87.93316553017848491 ) ) ;
#133793=VECTOR ( 'NONE', #120036, 1000.000000000000000 ) ;
#133797=DIRECTION ( 'NONE',  ( -0.5932847527679298016, -0.8049926720990051576, -5.621233785078291429E-15 ) ) ;
#133834=ORIENTED_EDGE ( 'NONE', *, *, #211451, .F. ) ;
#134095=CARTESIAN_POINT ( 'NONE',  ( 18.39999999999999503, 64.52683809664929981, -78.77310748452438816 ) ) ;
#134105=DIRECTION ( 'NONE',  ( -1.652117596168391700E-15, 1.000000000000000000, 6.982962677686266711E-15 ) ) ;
#134269=DIRECTION ( 'NONE',  ( -0.000000000000000000, -6.982962677686266711E-15, 1.000000000000000000 ) ) ;
#134492=EDGE_LOOP ( 'NONE', ( #138169, #140470, #226592, #204986 ) ) ;
#134569=EDGE_CURVE ( 'NONE', #76393, #91770, #199269, .T. ) ;
#134628=CARTESIAN_POINT ( 'NONE',  ( -16.92973740335347443, 66.00749618554451104, -90.42916651972677755 ) ) ;
#134665=AXIS2_PLACEMENT_3D ( 'NONE', #131673, #15615, #52122 ) ;
#134818=LINE ( 'NONE', #94425, #122469 ) ;
#134972=VECTOR ( 'NONE', #180314, 1000.000000000000000 ) ;
#135160=DIRECTION ( 'NONE',  ( 0.000000000000000000, 0.000000000000000000, 1.000000000000000000 ) ) ;
#135287=EDGE_CURVE ( 'NONE', #236175, #211977, #180081, .T. ) ;
#135349=DIRECTION ( 'NONE',  ( 0.000000000000000000, -1.000000000000000000, -6.982962677686266711E-15 ) ) ;
#135668=DIRECTION ( 'NONE',  ( -0.000000000000000000, -6.982962677686266711E-15, 1.000000000000000000 ) ) ;
#135876=VECTOR ( 'NONE', #64410, 1000.000000000000000 ) ;
#135900=DIRECTION ( 'NONE',  ( -1.073024830501117725E-15, -6.982962677686266711E-15, 1.000000000000000000 ) ) ;
#135923=EDGE_CURVE ( 'NONE', #66229, #249247, #102285, .T. ) ;
#135931=DIRECTION ( 'NONE',  ( 1.000000000000000000, 7.492892343619937423E-30, -1.073024830501117725E-15 ) ) ;
#136022=VERTEX_POINT ( 'NONE', #226098 ) ;
#136063=ORIENTED_EDGE ( 'NONE', *, *, #60768, .F. ) ;
#136216=CARTESIAN_POINT ( 'NONE',  ( -16.85697194749132422, 66.09145628588828458, -90.08810321691005640 ) ) ;
#136342=CARTESIAN_POINT ( 'NONE',  ( 17.23472005113827876, 65.69211804551110845, -91.56968434459304262 ) ) ;
#136453=LINE ( 'NONE', #197731, #195759 ) ;
#136626=UNCERTAINTY_MEASURE_WITH_UNIT (LENGTH_MEASURE( 1.000000000000000082E-05 ), #169937, 'distance_accuracy_value', 'NONE');
#136703=DIRECTION ( 'NONE',  ( -0.7071067811865456854, -0.7071067811865493491, -4.937700262164544098E-15 ) ) ;
#136912=DIRECTION ( 'NONE',  ( -1.000000000000000000, -0.000000000000000000, -0.000000000000000000 ) ) ;
#137217=CARTESIAN_POINT ( 'NONE',  ( -16.94878442675512886, 66.00827089702086425, -90.41132706016226450 ) ) ;
#137255=DIRECTION ( 'NONE',  ( 0.000000000000000000, 6.982962677686266711E-15, -1.000000000000000000 ) ) ;
#137498=ORIENTED_EDGE ( 'NONE', *, *, #116228, .F. ) ;
#137534=CARTESIAN_POINT ( 'NONE',  ( 16.87683809663750267, 66.05000000001187743, -90.37310748452438247 ) ) ;
#137586=AXIS2_PLACEMENT_3D ( 'NONE', #61501, #228, #141042 ) ;
#137752=CARTESIAN_POINT ( 'NONE',  ( -14.56336952470180357, 66.55335465531658201, -84.61230102842418432 ) ) ;
#137924=ADVANCED_FACE ( 'NONE', ( #231635 ), #252448, .F. ) ;
#138072=DIRECTION ( 'NONE',  ( -1.000000000000000000, 0.000000000000000000, 0.000000000000000000 ) ) ;
#138120=LINE ( 'NONE', #20782, #29446 ) ;
#138150=DIRECTION ( 'NONE',  ( -1.000000000000000000, -1.652117596168391700E-15, -1.153667551319263085E-29 ) ) ;
#138169=ORIENTED_EDGE ( 'NONE', *, *, #171466, .F. ) ;
#138431=CARTESIAN_POINT ( 'NONE',  ( -18.39999999999999858, 64.25000000001190870, -93.77310748452438816 ) ) ;
#138514=PLANE ( 'NONE',  #99006 ) ;
#138810=DIRECTION ( 'NONE',  ( -0.000000000000000000, -6.982962677686266711E-15, 1.000000000000000000 ) ) ;
#138815=DIRECTION ( 'NONE',  ( 0.000000000000000000, -0.9553114395362733990, 0.2956011730205631016 ) ) ;
#138823=EDGE_LOOP ( 'NONE', ( #104418, #50605, #103536, #105504 ) ) ;
#139012=CARTESIAN_POINT ( 'NONE',  ( -12.25000000000000178, 66.65000000001185754, -86.27310748452437394 ) ) ;
#139023=VERTEX_POINT ( 'NONE', #34778 ) ;
#139313=VECTOR ( 'NONE', #29220, 999.9999999999998863 ) ;
#139318=CARTESIAN_POINT ( 'NONE',  ( -16.94165728009537020, 66.01213024408802710, -82.13205247601418080 ) ) ;
#139377=CARTESIAN_POINT ( 'NONE',  ( -14.23072895065542909, 66.54401276639910634, -88.01157631762657729 ) ) ;
#139495=VECTOR ( 'NONE', #76702, 1000.000000000000000 ) ;
#139587=VERTEX_POINT ( 'NONE', #39616 ) ;
#139693=CARTESIAN_POINT ( 'NONE',  ( 18.39999999999999503, 64.52683809664938508, -90.37310748452438247 ) ) ;
#139818=FACE_OUTER_BOUND ( 'NONE', #58795, .T. ) ;
#139921=DIRECTION ( 'NONE',  ( -0.7071067811865456854, -0.7071067811865493491, -4.937700262164544098E-15 ) ) ;
#140006=CARTESIAN_POINT ( 'NONE',  ( -17.80356949363276087, 65.12326860301656950, -79.81003446029008330 ) ) ;
#140055=CARTESIAN_POINT ( 'NONE',  ( -16.96982749440706328, 66.05000000001182059, -82.64788589333610958 ) ) ;
#140083=CARTESIAN_POINT ( 'NONE',  ( 18.39999999999999503, 64.52683809664932824, -82.17310748452439384 ) ) ;
#140268=CARTESIAN_POINT ( 'NONE',  ( -16.94062896051973865, 66.00728089491119022, -90.42059094240558181 ) ) ;
#140326=AXIS2_PLACEMENT_3D ( 'NONE', #175956, #59801, #98923 ) ;
#140344=CARTESIAN_POINT ( 'NONE',  ( 21.72449340488910252, 65.71604372252073745, -90.37310748452436826 ) ) ;
#140357=CARTESIAN_POINT ( 'NONE',  ( 23.24999999999999645, 67.17743825834546101, -90.37310748452436826 ) ) ;
#140375=EDGE_LOOP ( 'NONE', ( #119990, #171974, #72355, #34682 ) ) ;
#140470=ORIENTED_EDGE ( 'NONE', *, *, #173356, .T. ) ;
#140552=DIRECTION ( 'NONE',  ( 0.000000000000000000, -1.000000000000000000, -6.982962677686266711E-15 ) ) ;
#140792=FACE_OUTER_BOUND ( 'NONE', #159281, .T. ) ;
#141042=DIRECTION ( 'NONE',  ( 1.000000000000000000, 0.000000000000000000, 0.000000000000000000 ) ) ;
#141170=FILL_AREA_STYLE ('',( #199875 ) ) ;
#141315=CARTESIAN_POINT ( 'NONE',  ( -17.29838795459062695, 65.62845014205868210, -80.91836620191291729 ) ) ;
#141360=CARTESIAN_POINT ( 'NONE',  ( -16.87333278164152972, 66.11739021543296246, -82.65627529067786838 ) ) ;
#141397=EDGE_CURVE ( 'NONE', #76393, #139587, #73382, .T. ) ;
#141539=ORIENTED_EDGE ( 'NONE', *, *, #12047, .T. ) ;
#141546=EDGE_CURVE ( 'NONE', #103638, #256979, #92798, .T. ) ;
#141614=ORIENTED_EDGE ( 'NONE', *, *, #52061, .F. ) ;
#141618=CARTESIAN_POINT ( 'NONE',  ( -14.87770893841227071, 66.56936289831506315, -84.75484686646342425 ) ) ;
#141684=ORIENTED_EDGE ( 'NONE', *, *, #258025, .F. ) ;
#141856=LINE ( 'NONE', #218818, #118235 ) ;
#141944=CARTESIAN_POINT ( 'NONE',  ( -16.87435696428308063, 66.04999753707964771, -90.37311571935781274 ) ) ;
#142115=EDGE_CURVE ( 'NONE', #76792, #201406, #60719, .T. ) ;
#142528=AXIS2_PLACEMENT_3D ( 'NONE', #176809, #34737, #193790 ) ;
#143012=ORIENTED_EDGE ( 'NONE', *, *, #211314, .T. ) ;
#143309=EDGE_CURVE ( 'NONE', #179202, #10328, #171309, .T. ) ;
#143379=ORIENTED_EDGE ( 'NONE', *, *, #154310, .T. ) ;
#143474=DIRECTION ( 'NONE',  ( -1.073024830501117725E-15, -6.982962677686266711E-15, 1.000000000000000000 ) ) ;
#143548=CARTESIAN_POINT ( 'NONE',  ( -16.86420534634261514, 66.02938455442009058, -82.10477093528699299 ) ) ;
#143750=LINE ( 'NONE', #9373, #250012 ) ;
#143857=CARTESIAN_POINT ( 'NONE',  ( -15.55912972643740488, 67.50912972644923116, -82.17310748452437963 ) ) ;
#143885=( BOUNDED_CURVE ( )  B_SPLINE_CURVE ( 3, ( #155885, #16366, #256170, #197541 ),
 .UNSPECIFIED., .F., .T. ) 
 B_SPLINE_CURVE_WITH_KNOTS ( ( 4, 4 ),
 ( 4.712388980384690562, 5.672655318024762749 ),
 .UNSPECIFIED. ) 
 CURVE ( )  GEOMETRIC_REPRESENTATION_ITEM ( )  RATIONAL_B_SPLINE_CURVE ( ( 1.000000000000000000, 0.9246222802177245237, 0.9246222802177245237, 1.000000000000000000 ) ) 
 REPRESENTATION_ITEM ( '' )  );
#144121=CARTESIAN_POINT ( 'NONE',  ( -16.93339986808596365, 65.99489607144595027, -90.45711381271152618 ) ) ;
#144240=DIRECTION ( 'NONE',  ( 1.000000000000000000, 0.000000000000000000, 0.000000000000000000 ) ) ;
#144274=LINE ( 'NONE', #163879, #18672 ) ;
#144564=VERTEX_POINT ( 'NONE', #17471 ) ;
#144726=CARTESIAN_POINT ( 'NONE',  ( -18.35668295345803713, 64.52683809664931402, -78.77310748452438816 ) ) ;
#144776=CARTESIAN_POINT ( 'NONE',  ( -16.77683809663752257, 66.05416425680765258, -82.18705650362858250 ) ) ;
#144823=CARTESIAN_POINT ( 'NONE',  ( -16.88460203013675454, 66.04524099677610138, -82.15721567498616196 ) ) ;
#144861=CARTESIAN_POINT ( 'NONE',  ( -23.25000000000000355, 65.95000000001186891, -90.27310748452438816 ) ) ;
#145155=LINE ( 'NONE', #224696, #4888 ) ;
#145199=CARTESIAN_POINT ( 'NONE',  ( -16.79270642812295833, 66.05375578307362616, -82.18417420596148304 ) ) ;
#145332=EDGE_CURVE ( 'NONE', #26497, #92572, #72, .T. ) ;
#145334=ORIENTED_EDGE ( 'NONE', *, *, #103832, .T. ) ;
#145394=CARTESIAN_POINT ( 'NONE',  ( -18.40000000000000213, 64.51332499825421962, -93.77310748452438816 ) ) ;
#145693=CARTESIAN_POINT ( 'NONE',  ( -16.94445028196807002, 66.00793639031407167, -82.13043766294282477 ) ) ;
#145699=ORIENTED_EDGE ( 'NONE', *, *, #12597, .F. ) ;
#146001=ORIENTED_EDGE ( 'NONE', *, *, #158365, .T. ) ;
#146227=CARTESIAN_POINT ( 'NONE',  ( -18.40000000000000213, 64.52683809664929981, -78.84905355133234650 ) ) ;
#146425=CARTESIAN_POINT ( 'NONE',  ( 15.74999999999999645, 66.65000000001185754, -86.27310748452437394 ) ) ;
#146638=ORIENTED_EDGE ( 'NONE', *, *, #104340, .F. ) ;
#146646=CARTESIAN_POINT ( 'NONE',  ( -20.65000000000000568, 70.35000000001181775, -82.17310748452435121 ) ) ;
#146787=CARTESIAN_POINT ( 'NONE',  ( -18.40000000000000213, 64.52683809664938508, -90.47310748452439100 ) ) ;
#146896=VERTEX_POINT ( 'NONE', #146646 ) ;
#146979=AXIS2_PLACEMENT_3D ( 'NONE', #102374, #243196, #3288 ) ;
#147163=VECTOR ( 'NONE', #139921, 1000.000000000000000 ) ;
#147314=ORIENTED_EDGE ( 'NONE', *, *, #126500, .T. ) ;
#147378=B_SPLINE_CURVE_WITH_KNOTS ( 'NONE', 3,
 ( #30413, #229888, #89075, #13414, #12147, #51210, #109921, #70839, #172532, #111219 ),
 .UNSPECIFIED., .F., .F.,
 ( 4, 2, 2, 2, 4 ),
 ( 5.329075035707888194E-16, 9.930191194501786309E-05, 0.0001986038238895028137, 0.0003972076477784323555, 0.0007944152955563318257 ),
 .UNSPECIFIED. ) ;
#147408=CARTESIAN_POINT ( 'NONE',  ( -16.86337532320260735, 66.02003279578745776, -82.07418301554156415 ) ) ;
#147629=ORIENTED_EDGE ( 'NONE', *, *, #209788, .F. ) ;
#147714=CARTESIAN_POINT ( 'NONE',  ( -16.94107738177415357, 65.98576071487524075, -90.47310748452439100 ) ) ;
#147726=ORIENTED_EDGE ( 'NONE', *, *, #61458, .F. ) ;
#147733=DIRECTION ( 'NONE',  ( 0.7071067811865456854, 0.7071067811865493491, 4.937700262164544098E-15 ) ) ;
#147742=CARTESIAN_POINT ( 'NONE',  ( 13.22461703343585526, 66.56333706821274632, -84.70007075222952153 ) ) ;
#147870=ORIENTED_EDGE ( 'NONE', *, *, #133298, .F. ) ;
#148034=CARTESIAN_POINT ( 'NONE',  ( -17.04761207306817283, 65.97354912661403148, -82.17310748452439384 ) ) ;
#148273=CARTESIAN_POINT ( 'NONE',  ( 23.04999999999999716, 67.17743825834546101, -90.37310748452436826 ) ) ;
#148725=CARTESIAN_POINT ( 'NONE',  ( -18.35663730107557257, 64.52609257350069072, -93.77310748452438816 ) ) ;
#148732=VERTEX_POINT ( 'NONE', #145693 ) ;
#148764=STYLED_ITEM ( 'NONE', ( #81166 ), #189925 ) ;
#148783=ORIENTED_EDGE ( 'NONE', *, *, #216038, .F. ) ;
#149014=CARTESIAN_POINT ( 'NONE',  ( -18.41431012584569160, 64.51252797080373114, -93.79634349762605439 ) ) ;
#149069=CARTESIAN_POINT ( 'NONE',  ( -16.81744102076748959, 66.05000000001182059, -82.17310748452439384 ) ) ;
#149391=EDGE_CURVE ( 'NONE', #232261, #17815, #35756, .T. ) ;
#149436=EDGE_CURVE ( 'NONE', #215091, #197810, #111508, .T. ) ;
#149569=CARTESIAN_POINT ( 'NONE',  ( -16.94107738177414291, 65.98576071487519812, -82.07310748452438531 ) ) ;
#149936=( BOUNDED_SURFACE ( )  B_SPLINE_SURFACE ( 3, 2, ( 
 ( #44787, #219550, #43508 ),
 ( #141315, #5626, #160898 ),
 ( #140006, #224688, #220841 ),
 ( #120499, #99587, #21394 ) ),
 .UNSPECIFIED., .F., .F., .F. ) 
 B_SPLINE_SURFACE_WITH_KNOTS ( ( 4, 4 ),
 ( 3, 3 ),
 ( 0.3000847527772385059, 0.5552748953338751958 ),
 ( 0.000000000000000000, 1.000000000000000000 ),
 .UNSPECIFIED. ) 
 GEOMETRIC_REPRESENTATION_ITEM ( )  RATIONAL_B_SPLINE_SURFACE ( (
 ( 1.000000000000000000, 0.9152888060719408525, 1.000000000000000000),
 ( 1.000000000000000000, 0.9104333467450348438, 1.000000000000000000),
 ( 1.000000000000000000, 0.9035312726220574575, 1.000000000000000000),
 ( 1.000000000000000000, 0.8946697475932264831, 1.000000000000000000) ) ) 
 REPRESENTATION_ITEM ( '' )  SURFACE ( )  );
#150279=EDGE_CURVE ( 'NONE', #247441, #14757, #157674, .T. ) ;
#150340=( NAMED_UNIT ( * ) PLANE_ANGLE_UNIT ( ) SI_UNIT ( $, .RADIAN. ) );
#150365=CARTESIAN_POINT ( 'NONE',  ( 20.04999999999999716, 67.25000000001185185, -90.37310748452436826 ) ) ;
#150851=CARTESIAN_POINT ( 'NONE',  ( -16.87036670365549895, 66.01058118071021852, -90.50266760182643111 ) ) ;
#150954=DIRECTION ( 'NONE',  ( 0.000000000000000000, -1.000000000000000000, -6.982962677686266711E-15 ) ) ;
#150992=LINE ( 'NONE', #154862, #232996 ) ;
#151176=CARTESIAN_POINT ( 'NONE',  ( -17.22361732159832215, 65.65484434140945780, -91.65232295865725121 ) ) ;
#151222=ORIENTED_EDGE ( 'NONE', *, *, #141397, .F. ) ;
#151310=EDGE_CURVE ( 'NONE', #10053, #34828, #254275, .T. ) ;
#151320=VECTOR ( 'NONE', #64896, 1000.000000000000000 ) ;
#151436=EDGE_LOOP ( 'NONE', ( #76203, #231291, #171902, #54804 ) ) ;
#151971=CARTESIAN_POINT ( 'NONE',  ( 12.60053434924909865, 66.61046543766512684, -87.34829818013440672 ) ) ;
#152071=UNCERTAINTY_MEASURE_WITH_UNIT (LENGTH_MEASURE( 1.000000000000000082E-05 ), #358, 'distance_accuracy_value', 'NONE');
#152250=ORIENTED_EDGE ( 'NONE', *, *, #88603, .F. ) ;
#152310=CARTESIAN_POINT ( 'NONE',  ( -16.83199318825828072, 66.06935387203064636, -82.29552229631519822 ) ) ;
#152354=DIRECTION ( 'NONE',  ( 0.000000000000000000, -6.982962677686266711E-15, 1.000000000000000000 ) ) ;
#152451=DIRECTION ( 'NONE',  ( 1.000000000000000000, 0.000000000000000000, 0.000000000000000000 ) ) ;
#152463=ORIENTED_EDGE ( 'NONE', *, *, #20164, .T. ) ;
#152623=VECTOR ( 'NONE', #129804, 1000.000000000000000 ) ;
#152663=LINE ( 'NONE', #130488, #232697 ) ;
#152677=( GEOMETRIC_REPRESENTATION_CONTEXT ( 3 ) GLOBAL_UNCERTAINTY_ASSIGNED_CONTEXT ( ( #136626 ) ) GLOBAL_UNIT_ASSIGNED_CONTEXT ( ( #169937, #26540, #9518 ) ) REPRESENTATION_CONTEXT ( 'NONE', 'WORKASPACE' ) );
#153513=CARTESIAN_POINT ( 'NONE',  ( 0.000000000000000000, 0.000000000000000000, 0.000000000000000000 ) ) ;
#153515=VERTEX_POINT ( 'NONE', #195719 ) ;
#153574=VERTEX_POINT ( 'NONE', #217792 ) ;
#153623=CARTESIAN_POINT ( 'NONE',  ( -16.88328101497759448, 66.04964716579294759, -82.17192796959510304 ) ) ;
#153652=EDGE_CURVE ( 'NONE', #136022, #228701, #238666, .T. ) ;
#153779=ORIENTED_EDGE ( 'NONE', *, *, #168813, .F. ) ;
#153813=ORIENTED_EDGE ( 'NONE', *, *, #3416, .F. ) ;
#153886=CARTESIAN_POINT ( 'NONE',  ( -13.12432614554023402, 66.56923500458954379, -87.79257008977393184 ) ) ;
#153987=ORIENTED_EDGE ( 'NONE', *, *, #91706, .T. ) ;
#154250=VECTOR ( 'NONE', #200298, 1000.000000000000000 ) ;
#154283=EDGE_CURVE ( 'NONE', #10718, #100827, #196362, .T. ) ;
#154310=EDGE_CURVE ( 'NONE', #162722, #27378, #18987, .T. ) ;
#154348=EDGE_CURVE ( 'NONE', #119515, #69522, #130057, .T. ) ;
#154451=DIRECTION ( 'NONE',  ( -1.000000000000000000, -0.000000000000000000, -0.000000000000000000 ) ) ;
#154608=ORIENTED_EDGE ( 'NONE', *, *, #234512, .F. ) ;
#154688=EDGE_CURVE ( 'NONE', #27378, #191238, #256463, .T. ) ;
#154693=ORIENTED_EDGE ( 'NONE', *, *, #7851, .F. ) ;
#154862=CARTESIAN_POINT ( 'NONE',  ( -12.25000000000000178, 66.15000000001185754, -86.27310748452437394 ) ) ;
#154882=CARTESIAN_POINT ( 'NONE',  ( -16.89081410710458542, 66.04868147016469493, -82.16870156468802122 ) ) ;
#155152=CARTESIAN_POINT ( 'NONE',  ( -15.74999999999999645, 66.65000000001187175, -86.50158811269930936 ) ) ;
#155178=DIRECTION ( 'NONE',  ( 1.000000000000000000, 0.000000000000000000, 0.000000000000000000 ) ) ;
#155837=CARTESIAN_POINT ( 'NONE',  ( -16.89155683852331791, 66.05000000001187743, -89.74573563498417172 ) ) ;
#155885=CARTESIAN_POINT ( 'NONE',  ( -17.11825945287482753, 65.95000000001188312, -90.37310748452438247 ) ) ;
#156034=CARTESIAN_POINT ( 'NONE',  ( -23.25000000000000355, 70.35000000001181775, -82.17310748452435121 ) ) ;
#156201=DIRECTION ( 'NONE',  ( -1.000000000000000000, 0.000000000000000000, 0.000000000000000000 ) ) ;
#156224=AXIS2_PLACEMENT_3D ( 'NONE', #148273, #49166, #247360 ) ;
#156728=ORIENTED_EDGE ( 'NONE', *, *, #59591, .T. ) ;
#156765=EDGE_LOOP ( 'NONE', ( #24197, #192388, #141684, #178438 ) ) ;
#156768=( GEOMETRIC_REPRESENTATION_CONTEXT ( 3 ) GLOBAL_UNCERTAINTY_ASSIGNED_CONTEXT ( ( #79213 ) ) GLOBAL_UNIT_ASSIGNED_CONTEXT ( ( #209015, #150340, #109897 ) ) REPRESENTATION_CONTEXT ( 'NONE', 'WORKASPACE' ) );
#156785=DIRECTION ( 'NONE',  ( 0.000000000000000000, 1.000000000000000000, 0.000000000000000000 ) ) ;
#156978=CARTESIAN_POINT ( 'NONE',  ( -16.90257928357874562, 66.04589317890649625, -90.38682205441068618 ) ) ;
#157053=EDGE_LOOP ( 'NONE', ( #178982, #115431, #12308, #68432, #229456 ) ) ;
#157373=CARTESIAN_POINT ( 'NONE',  ( -14.11361717019516071, 66.54257354752292031, -84.52306561612432745 ) ) ;
#157460=ADVANCED_FACE ( 'NONE', ( #15090 ), #16385, .T. ) ;
#157642=DIRECTION ( 'NONE',  ( -1.186688945009010077E-16, -1.000000000000000000, -6.789366196018717631E-15 ) ) ;
#157655=CARTESIAN_POINT ( 'NONE',  ( -12.25000000000000178, 66.15000000001185754, -86.27310748452437394 ) ) ;
#157674=LINE ( 'NONE', #179773, #177959 ) ;
#157749=ORIENTED_EDGE ( 'NONE', *, *, #154688, .F. ) ;
#157788=CARTESIAN_POINT ( 'NONE',  ( -21.64999999999999858, 65.95000000001186891, -90.27310748452438816 ) ) ;
#157836=ORIENTED_EDGE ( 'NONE', *, *, #83625, .F. ) ;
#157873=EDGE_CURVE ( 'NONE', #2966, #26113, #110380, .T. ) ;
#157881=ORIENTED_EDGE ( 'NONE', *, *, #203329, .F. ) ;
#158116=CARTESIAN_POINT ( 'NONE',  ( 18.39999999999997371, 64.52683809664929981, -78.77310748452438816 ) ) ;
#158245=VECTOR ( 'NONE', #168438, 1000.000000000000000 ) ;
#158263=ORIENTED_EDGE ( 'NONE', *, *, #60851, .T. ) ;
#158279=CARTESIAN_POINT ( 'NONE',  ( -16.93658623642905070, 66.01961832835475263, -90.41120475539514700 ) ) ;
#158365=EDGE_CURVE ( 'NONE', #56902, #202204, #127324, .T. ) ;
#158417=CARTESIAN_POINT ( 'NONE',  ( -16.84793658983426923, 66.05000000001189164, -90.28946080671389041 ) ) ;
#158997=CARTESIAN_POINT ( 'NONE',  ( -14.87779219673428521, 66.56936653093906386, -87.79134168970027474 ) ) ;
#159015=EDGE_CURVE ( 'NONE', #211977, #179202, #91745, .T. ) ;
#159281=EDGE_LOOP ( 'NONE', ( #215828, #69962, #114669, #234096 ) ) ;
#159569=ADVANCED_FACE ( 'NONE', ( #19428 ), #37728, .F. ) ;
#159651=CARTESIAN_POINT ( 'NONE',  ( -16.87683809663752399, 66.13411015067987364, -82.79053429159371547 ) ) ;
#159879=CARTESIAN_POINT ( 'NONE',  ( -16.93906926870270624, 65.98785312906531431, -90.46965517729756812 ) ) ;
#160238=CARTESIAN_POINT ( 'NONE',  ( -16.92507428761700439, 66.05000000001182059, -82.23650494414594903 ) ) ;
#160405=DIRECTION ( 'NONE',  ( 0.000000000000000000, 6.982962677686266711E-15, -1.000000000000000000 ) ) ;
#160442=ADVANCED_FACE ( 'NONE', ( #42224 ), #149936, .T. ) ;
#160499=ORIENTED_EDGE ( 'NONE', *, *, #154283, .T. ) ;
#160898=CARTESIAN_POINT ( 'NONE',  ( -17.22767730083791804, 65.65075578754621688, -80.88067879395967452 ) ) ;
#160914=ORIENTED_EDGE ( 'NONE', *, *, #123244, .F. ) ;
#160924=CARTESIAN_POINT ( 'NONE',  ( -16.77779411440718604, 66.05389855290421508, -82.18616490152891174 ) ) ;
#161125=ORIENTED_EDGE ( 'NONE', *, *, #188749, .T. ) ;
#161128=DIRECTION ( 'NONE',  ( 1.000000000000000000, 0.000000000000000000, 0.000000000000000000 ) ) ;
#161137=VECTOR ( 'NONE', #38239, 1000.000000000000000 ) ;
#161573=DIRECTION ( 'NONE',  ( -1.000000000000000000, 1.646408749285563322E-14, -1.073024830501002749E-15 ) ) ;
#161581=CARTESIAN_POINT ( 'NONE',  ( -16.77828822508139694, 66.05377062509111852, -90.36047923315042851 ) ) ;
#161591=ADVANCED_FACE ( 'NONE', ( #43555, #25283, #21441 ), #222150, .T. ) ;
#161674=CARTESIAN_POINT ( 'NONE',  ( -18.40000000000000213, 64.52683809664929981, -78.84905355133234650 ) ) ;
#161761=DIRECTION ( 'NONE',  ( -1.073024830501117725E-15, 6.982962677686266711E-15, -1.000000000000000000 ) ) ;
#161815=VERTEX_POINT ( 'NONE', #11537 ) ;
#162337=DIRECTION ( 'NONE',  ( -1.000000000000000000, 0.000000000000000000, -0.000000000000000000 ) ) ;
#162488=CARTESIAN_POINT ( 'NONE',  ( -12.92414019175886430, 66.58236703690553782, -84.87415901879208491 ) ) ;
#162695=EDGE_CURVE ( 'NONE', #161815, #231129, #32957, .T. ) ;
#162722=VERTEX_POINT ( 'NONE', #161674 ) ;
#162767=DIRECTION ( 'NONE',  ( 1.000000000000000000, 0.000000000000000000, 0.000000000000000000 ) ) ;
#162864=CARTESIAN_POINT ( 'NONE',  ( -16.79814274880124358, 66.05072745733455974, -90.37067444747638945 ) ) ;
#163071=CARTESIAN_POINT ( 'NONE',  ( 20.73486653747088937, 68.25000000001183764, -90.37310748452435405 ) ) ;
#163145=CARTESIAN_POINT ( 'NONE',  ( -16.97683809663753252, 66.05000000001190585, -89.75158271585443970 ) ) ;
#163367=CARTESIAN_POINT ( 'NONE',  ( -16.27683809663750480, 66.65000000001182912, -82.07310748452438531 ) ) ;
#163600=ADVANCED_FACE ( 'NONE', ( #204006 ), #121919, .F. ) ;
#163879=CARTESIAN_POINT ( 'NONE',  ( -20.65000000000000568, 68.75000000001189449, -93.77310748452435973 ) ) ;
#164306=EDGE_LOOP ( 'NONE', ( #247637, #48680, #226053, #128776, #76690, #100145 ) ) ;
#164409=ORIENTED_EDGE ( 'NONE', *, *, #145332, .F. ) ;
#164450=DIRECTION ( 'NONE',  ( 1.000000000000000000, 0.000000000000000000, 0.000000000000000000 ) ) ;
#164474=CARTESIAN_POINT ( 'NONE',  ( -16.77683809663752257, 66.05416425680765258, -82.18705650362858250 ) ) ;
#164664=ORIENTED_EDGE ( 'NONE', *, *, #107211, .T. ) ;
#164756=FILL_AREA_STYLE ('',( #68222 ) ) ;
#164810=CARTESIAN_POINT ( 'NONE',  ( -16.77308656112214535, 66.05000000001189164, -90.37291429282207389 ) ) ;
#164915=CIRCLE ( 'NONE', #39496, 1.749999999999998002 ) ;
#165234=CARTESIAN_POINT ( 'NONE',  ( 18.39999999999999503, 64.25000000001179501, -78.77310748452438816 ) ) ;
#165256=CARTESIAN_POINT ( 'NONE',  ( -17.78043020864321022, 65.14640788800610949, -79.86005831880416395 ) ) ;
#165330=ORIENTED_EDGE ( 'NONE', *, *, #87499, .F. ) ;
#165366=EDGE_CURVE ( 'NONE', #202204, #117904, #62675, .T. ) ;
#165465=ORIENTED_EDGE ( 'NONE', *, *, #88603, .T. ) ;
#165549=ORIENTED_EDGE ( 'NONE', *, *, #75642, .T. ) ;
#165564=VECTOR ( 'NONE', #85826, 1000.000000000000000 ) ;
#165629=DIRECTION ( 'NONE',  ( -1.000000000000000000, 0.000000000000000000, 0.000000000000000000 ) ) ;
#165719=CARTESIAN_POINT ( 'NONE',  ( -16.90137573187934095, 66.05000000001189164, -90.23469006042749641 ) ) ;
#165728=ORIENTED_EDGE ( 'NONE', *, *, #229780, .T. ) ;
#166099=ADVANCED_FACE ( 'NONE', ( #4301 ), #40268, .T. ) ;
#166129=CARTESIAN_POINT ( 'NONE',  ( -16.79270642812297609, 66.05375578307368301, -90.36204076308727906 ) ) ;
#166142=AXIS2_PLACEMENT_3D ( 'NONE', #88747, #11833, #87469 ) ;
#166178=DIRECTION ( 'NONE',  ( 1.000000000000000000, 0.000000000000000000, 0.000000000000000000 ) ) ;
#166382=EDGE_LOOP ( 'NONE', ( #74789, #192647, #17231, #207281, #32740 ) ) ;
#166471=CARTESIAN_POINT ( 'NONE',  ( -16.97092634996643667, 65.99911103366365239, -82.15325025082218247 ) ) ;
#166661=CIRCLE ( 'NONE', #45818, 0.9000000000000014655 ) ;
#167003=EDGE_CURVE ( 'NONE', #146896, #14013, #66256, .T. ) ;
#167116=ORIENTED_EDGE ( 'NONE', *, *, #106507, .T. ) ;
#167251=ORIENTED_EDGE ( 'NONE', *, *, #3065, .T. ) ;
#167299=CARTESIAN_POINT ( 'NONE',  ( -18.44085059012131822, 64.48598750652809031, -93.76341280364593445 ) ) ;
#167376=CARTESIAN_POINT ( 'NONE',  ( -16.80070461187904840, 66.05000000001183480, -82.17007131368336559 ) ) ;
#167535=CIRCLE ( 'NONE', #71668, 0.1000000000000028644 ) ;
#167750=CARTESIAN_POINT ( 'NONE',  ( -17.01764560440361507, 66.05000000001182059, -82.27310748373757576 ) ) ;
#167936=CARTESIAN_POINT ( 'NONE',  ( 20.73486653747088582, 68.75000000001183764, -90.37310748452435405 ) ) ;
#167952=CARTESIAN_POINT ( 'NONE',  ( -20.65000000000000568, 68.75000000001182343, -82.17310748452436542 ) ) ;
#167994=CARTESIAN_POINT ( 'NONE',  ( -17.11825945287481332, 65.95000000001181206, -82.17310748452439384 ) ) ;
#168253=ORIENTED_EDGE ( 'NONE', *, *, #114999, .F. ) ;
#168438=DIRECTION ( 'NONE',  ( 0.000000000000000000, -1.000000000000000000, -6.982962677686266711E-15 ) ) ;
#168639=CARTESIAN_POINT ( 'NONE',  ( 12.42718393586866021, 66.62934494888835957, -85.49728422854349219 ) ) ;
#168813=EDGE_CURVE ( 'NONE', #26102, #216777, #196034, .T. ) ;
#168857=ORIENTED_EDGE ( 'NONE', *, *, #118529, .F. ) ;
#168889=CARTESIAN_POINT ( 'NONE',  ( -16.87331047859649757, 66.05000000001182059, -82.17310748452439384 ) ) ;
#168973=DIRECTION ( 'NONE',  ( 0.000000000000000000, 0.9553114395362733990, 0.2956011730205631016 ) ) ;
#169243=CARTESIAN_POINT ( 'NONE',  ( 18.39999999999999503, 64.25000000001188027, -90.37310748452439668 ) ) ;
#169279=CARTESIAN_POINT ( 'NONE',  ( -16.97683809663752186, 66.15000000001182912, -82.92547150272069700 ) ) ;
#169411=VERTEX_POINT ( 'NONE', #208287 ) ;
#169567=PLANE ( 'NONE',  #134665 ) ;
#169570=CARTESIAN_POINT ( 'NONE',  ( -20.65000000000000568, 68.75000000001189449, -93.77310748452435973 ) ) ;
#169630=PRODUCT_DEFINITION_FORMATION_WITH_SPECIFIED_SOURCE ( 'ANY', '', #28562, .NOT_KNOWN. ) ;
#169710=CARTESIAN_POINT ( 'NONE',  ( -23.25000000000000355, 70.35000000001181775, -82.17310748452435121 ) ) ;
#169881=EDGE_CURVE ( 'NONE', #65335, #100827, #134818, .T. ) ;
#169937=( LENGTH_UNIT ( ) NAMED_UNIT ( * ) SI_UNIT ( .MILLI., .METRE. ) );
#170110=CARTESIAN_POINT ( 'NONE',  ( -16.87683809663752399, 54.76195096157879760, -90.37310748452445353 ) ) ;
#170272=CARTESIAN_POINT ( 'NONE',  ( 15.52844286134407525, 66.62433047358608462, -87.15531747513846028 ) ) ;
#170289=CARTESIAN_POINT ( 'NONE',  ( -16.94107738177414291, 65.98576071487519812, -82.07310748452438531 ) ) ;
#170555=CARTESIAN_POINT ( 'NONE',  ( 18.54999999999999716, 66.05000000001186322, -90.37310748452443931 ) ) ;
#170641=LINE ( 'NONE', #211001, #129891 ) ;
#170675=ORIENTED_EDGE ( 'NONE', *, *, #44023, .T. ) ;
#170915=LINE ( 'NONE', #112195, #3075 ) ;
#171198=CARTESIAN_POINT ( 'NONE',  ( 15.31784899511110076, 66.60336962369413527, -85.11605009170608582 ) ) ;
#171309=( BOUNDED_CURVE ( )  B_SPLINE_CURVE ( 3, ( #37382, #99866, #179461, #765 ),
 .UNSPECIFIED., .F., .F. ) 
 B_SPLINE_CURVE_WITH_KNOTS ( ( 4, 4 ),
 ( 0.3000847527772370071, 0.5497968875596818128 ),
 .UNSPECIFIED. ) 
 CURVE ( )  GEOMETRIC_REPRESENTATION_ITEM ( )  RATIONAL_B_SPLINE_CURVE ( ( 1.000000000000000000, 0.9948104011409419911, 0.9948104011409419911, 1.000000000000000000 ) ) 
 REPRESENTATION_ITEM ( '' )  );
#171342=DIRECTION ( 'NONE',  ( -1.000000000000000000, 0.000000000000000000, 0.000000000000000000 ) ) ;
#171422=ORIENTED_EDGE ( 'NONE', *, *, #230496, .F. ) ;
#171437=ORIENTED_EDGE ( 'NONE', *, *, #68258, .T. ) ;
#171466=EDGE_CURVE ( 'NONE', #245034, #92834, #69501, .T. ) ;
#171802=CIRCLE ( 'NONE', #92646, 0.09999999999999939493 ) ;
#171888=CARTESIAN_POINT ( 'NONE',  ( -16.89268316805465986, 66.04827818676963602, -82.16735500597883401 ) ) ;
#171902=ORIENTED_EDGE ( 'NONE', *, *, #171466, .T. ) ;
#171974=ORIENTED_EDGE ( 'NONE', *, *, #44023, .F. ) ;
#171981=CARTESIAN_POINT ( 'NONE',  ( 20.27550659511088682, 66.78395627750303731, -93.77310748452437394 ) ) ;
#172016=CARTESIAN_POINT ( 'NONE',  ( 12.25000000000000000, 66.15000000001185754, -86.27310748452437394 ) ) ;
#172225=SHAPE_DEFINITION_REPRESENTATION ( #114014, #125202 ) ;
#172487=CARTESIAN_POINT ( 'NONE',  ( 15.69410316191959254, 66.64325398293360081, -85.81974776316017994 ) ) ;
#172532=CARTESIAN_POINT ( 'NONE',  ( -16.97683809663753607, 66.05000000001183480, -82.79463665241381420 ) ) ;
#172542=CARTESIAN_POINT ( 'NONE',  ( 21.72449340488910607, 65.71604372252076587, -93.77310748452438816 ) ) ;
#172757=B_SPLINE_CURVE_WITH_KNOTS ( 'NONE', 3,
 ( #241926, #24190, #26770, #145394 ),
 .UNSPECIFIED., .F., .F.,
 ( 4, 4 ),
 ( 0.000000000000000000, 7.713889350929220882E-05 ),
 .UNSPECIFIED. ) ;
#172776=DIRECTION ( 'NONE',  ( -1.000000000000000000, 1.646408749285562691E-14, 1.149681084847720908E-28 ) ) ;
#172859=CARTESIAN_POINT ( 'NONE',  ( -16.94445028196807002, 66.00793639031407167, -82.13043766294282477 ) ) ;
#172867=ORIENTED_EDGE ( 'NONE', *, *, #162695, .T. ) ;
#173356=EDGE_CURVE ( 'NONE', #245034, #77679, #257674, .T. ) ;
#173359=ORIENTED_EDGE ( 'NONE', *, *, #173852, .T. ) ;
#173434=CARTESIAN_POINT ( 'NONE',  ( -14.77538296656415184, 66.56333706821271790, -84.70007075222947890 ) ) ;
#173490=ORIENTED_EDGE ( 'NONE', *, *, #241961, .F. ) ;
#173750=DIRECTION ( 'NONE',  ( -1.020425574104004196E-15, 6.982962677686266711E-15, -1.000000000000000000 ) ) ;
#173852=EDGE_CURVE ( 'NONE', #255984, #177874, #170915, .T. ) ;
#173868=ORIENTED_EDGE ( 'NONE', *, *, #243343, .T. ) ;
#173965=ORIENTED_EDGE ( 'NONE', *, *, #149391, .T. ) ;
#174551=DIRECTION ( 'NONE',  ( -0.000000000000000000, -6.982962677686266711E-15, 1.000000000000000000 ) ) ;
#174731=CARTESIAN_POINT ( 'NONE',  ( -12.25000000000000178, 66.65000000001185754, -86.27310748452437394 ) ) ;
#174752=FACE_OUTER_BOUND ( 'NONE', #255018, .T. ) ;
#174857=LINE ( 'NONE', #229647, #107372 ) ;
#175117=CARTESIAN_POINT ( 'NONE',  ( -16.89797118371604867, 66.02361927736649250, -90.46040085208208836 ) ) ;
#175408=CARTESIAN_POINT ( 'NONE',  ( -16.87683809663750623, 66.05000000001187743, -89.62074346632789457 ) ) ;
#175443=DIRECTION ( 'NONE',  ( 0.000000000000000000, -6.982962677686266711E-15, 1.000000000000000000 ) ) ;
#175585=LINE ( 'NONE', #217238, #92763 ) ;
#175775=APPLICATION_CONTEXT ( 'automotive_design' ) ;
#175797=CARTESIAN_POINT ( 'NONE',  ( -18.34374000495059676, 64.52683809664929981, -78.77310748452438816 ) ) ;
#175956=CARTESIAN_POINT ( 'NONE',  ( 18.39999999999999503, 70.35000000001187459, -90.37310748452433984 ) ) ;
#175964=ORIENTED_EDGE ( 'NONE', *, *, #103832, .F. ) ;
#175986=CARTESIAN_POINT ( 'NONE',  ( -14.77738660682463312, 66.56344716000744199, -87.84515201176407118 ) ) ;
#176213=ORIENTED_EDGE ( 'NONE', *, *, #113774, .T. ) ;
#176239=ORIENTED_EDGE ( 'NONE', *, *, #241570, .T. ) ;
#176284=ORIENTED_EDGE ( 'NONE', *, *, #116228, .T. ) ;
#176310=EDGE_CURVE ( 'NONE', #249247, #136022, #136453, .T. ) ;
#176359=LINE ( 'NONE', #172542, #63820 ) ;
#176392=CARTESIAN_POINT ( 'NONE',  ( -16.97683809663752186, 66.05000000001190585, -93.77310748452438816 ) ) ;
#176472=LINE ( 'NONE', #255929, #46489 ) ;
#176809=CARTESIAN_POINT ( 'NONE',  ( -17.11825945287481332, 65.95000000001181206, -82.27310748452437394 ) ) ;
#176852=CARTESIAN_POINT ( 'NONE',  ( -21.65000000000000213, 68.75000000001188027, -90.37310748452435405 ) ) ;
#176894=CARTESIAN_POINT ( 'NONE',  ( 21.72449340488910252, 65.71604372252073745, -90.37310748452436826 ) ) ;
#177016=CARTESIAN_POINT ( 'NONE',  ( -16.88853107394619357, 66.04912151666482600, -82.17017113763215264 ) ) ;
#177166=EDGE_CURVE ( 'NONE', #189338, #11593, #75956, .T. ) ;
#177195=CARTESIAN_POINT ( 'NONE',  ( -16.77683809663752257, 52.34166666667851331, -86.27310748452447342 ) ) ;
#177390=CARTESIAN_POINT ( 'NONE',  ( -33.72168855820452649, 64.52683809664941350, -93.77310748452440237 ) ) ;
#177482=DIRECTION ( 'NONE',  ( 0.7071067811865493491, -0.7071067811865456854, -4.937700262164518065E-15 ) ) ;
#177835=CARTESIAN_POINT ( 'NONE',  ( -16.87683809663752399, 66.05000000001187743, -90.37310748452438247 ) ) ;
#177874=VERTEX_POINT ( 'NONE', #65661 ) ;
#177959=VECTOR ( 'NONE', #97623, 1000.000000000000000 ) ;
#177960=CARTESIAN_POINT ( 'NONE',  ( -16.84981964351479178, 66.08268176591317911, -90.15350587050488684 ) ) ;
#178074=EDGE_LOOP ( 'NONE', ( #185674, #15826, #94594, #69441 ) ) ;
#178169=VECTOR ( 'NONE', #216918, 1000.000000000000000 ) ;
#178213=CARTESIAN_POINT ( 'NONE',  ( -12.30589683808040391, 66.64325398293358660, -85.81974776316017994 ) ) ;
#178294=DIRECTION ( 'NONE',  ( -1.000000000000000000, 7.492892343619937423E-30, -1.073024830501117725E-15 ) ) ;
#178438=ORIENTED_EDGE ( 'NONE', *, *, #19572, .F. ) ;
#178442=CYLINDRICAL_SURFACE ( 'NONE', #129611, 0.1000000000000050432 ) ;
#178534=FACE_OUTER_BOUND ( 'NONE', #851, .T. ) ;
#178584=CARTESIAN_POINT ( 'NONE',  ( -16.77683809663752257, 66.05416425680770942, -90.35915846542016538 ) ) ;
#178982=ORIENTED_EDGE ( 'NONE', *, *, #211314, .F. ) ;
#179120=CARTESIAN_POINT ( 'NONE',  ( -16.94333152886235894, 66.00965798856138633, -90.41513901557878796 ) ) ;
#179202=VERTEX_POINT ( 'NONE', #212933 ) ;
#179255=CARTESIAN_POINT ( 'NONE',  ( -16.92280123533699410, 66.05000000001187743, -90.17247517043927019 ) ) ;
#179449=VERTEX_POINT ( 'NONE', #65403 ) ;
#179461=CARTESIAN_POINT ( 'NONE',  ( -17.78043020864320667, 65.14640788800619475, -92.68615665024458394 ) ) ;
#179576=ORIENTED_EDGE ( 'NONE', *, *, #118304, .T. ) ;
#179632=VECTOR ( 'NONE', #107533, 1000.000000000000000 ) ;
#179734=ORIENTED_EDGE ( 'NONE', *, *, #75687, .F. ) ;
#179766=CARTESIAN_POINT ( 'NONE',  ( -16.93301857435212199, 66.02369064527634634, -82.13733191336294226 ) ) ;
#179773=CARTESIAN_POINT ( 'NONE',  ( 20.05000000000002913, 68.75000000001186606, -93.77310748452435973 ) ) ;
#179830=CARTESIAN_POINT ( 'NONE',  ( -13.22483237240078147, 66.56332574816900660, -87.84624555352516495 ) ) ;
#179844=EDGE_LOOP ( 'NONE', ( #165330, #87626, #34270, #153779 ) ) ;
#179853=CARTESIAN_POINT ( 'NONE',  ( -16.81095280782811230, 66.05000000001187743, -90.37310748452526354 ) ) ;
#179900=CARTESIAN_POINT ( 'NONE',  ( 16.87683809663749557, 66.05000000001183480, -82.17310748452439384 ) ) ;
#180081=B_SPLINE_CURVE_WITH_KNOTS ( 'NONE', 3,
 ( #196087, #156978, #17437, #197354, #96939, #158279, #237774, #179120, #222030, #182953 ),
 .UNSPECIFIED., .F., .F.,
 ( 4, 3, 3, 4 ),
 ( 1.891637802867244836E-15, 3.877043166999269576E-05, 7.336897548475566824E-05, 7.659383120239756379E-05 ),
 .UNSPECIFIED. ) ;
#180172=EDGE_CURVE ( 'NONE', #200313, #110820, #203606, .T. ) ;
#180259=CARTESIAN_POINT ( 'NONE',  ( -16.87368910959167678, 66.03872618332046329, -90.41061438788379689 ) ) ;
#180314=DIRECTION ( 'NONE',  ( -1.000000000000000000, 0.000000000000000000, -0.000000000000000000 ) ) ;
#180353=VECTOR ( 'NONE', #135349, 1000.000000000000000 ) ;
#180541=AXIS2_PLACEMENT_3D ( 'NONE', #170110, #249611, #70991 ) ;
#180581=DIRECTION ( 'NONE',  ( -1.020425574104004196E-15, -6.982962677686266711E-15, 1.000000000000000000 ) ) ;
#180758=CARTESIAN_POINT ( 'NONE',  ( -12.60829076262180237, 66.61047060254509233, -85.20599957163069860 ) ) ;
#180954=ORIENTED_EDGE ( 'NONE', *, *, #188389, .F. ) ;
#181131=LINE ( 'NONE', #81974, #40692 ) ;
#181662=B_SPLINE_CURVE_WITH_KNOTS ( 'NONE', 3,
 ( #206118, #6623, #11798, #148725, #47019, #27523, #7929 ),
 .UNSPECIFIED., .F., .F.,
 ( 4, 3, 4 ),
 ( 0.000000000000000000, 4.520325912680429745E-05, 5.794988040901229230E-05 ),
 .UNSPECIFIED. ) ;
#182040=CARTESIAN_POINT ( 'NONE',  ( -15.39126916658602973, 66.61042836546539547, -85.20546677215520504 ) ) ;
#182150=ORIENTED_EDGE ( 'NONE', *, *, #59423, .T. ) ;
#182265=CARTESIAN_POINT ( 'NONE',  ( -20.65000000000000568, 70.35000000001190301, -93.77310748452434552 ) ) ;
#182495=DIRECTION ( 'NONE',  ( 1.000000000000000000, -7.125593699324843413E-30, 1.020425574104004196E-15 ) ) ;
#182797=DIRECTION ( 'NONE',  ( 1.186688945009009831E-16, 1.000000000000000000, 6.982962677686266711E-15 ) ) ;
#182953=CARTESIAN_POINT ( 'NONE',  ( -16.94445028196808778, 66.00793639031412852, -90.41577730610593733 ) ) ;
#183135=CARTESIAN_POINT ( 'NONE',  ( -16.87036670365549895, 65.91505003675658259, -90.47310748452439100 ) ) ;
#183276=CARTESIAN_POINT ( 'NONE',  ( -16.93909480342659890, 66.00692163521031830, -90.42276046785205779 ) ) ;
#183974=CARTESIAN_POINT ( 'NONE',  ( -16.94225986326250677, 66.05000000001189164, -90.07638810891651815 ) ) ;
#184268=DIRECTION ( 'NONE',  ( 1.073024830501117725E-15, -6.982962677686266711E-15, 1.000000000000000000 ) ) ;
#184325=DIRECTION ( 'NONE',  ( 0.000000000000000000, -6.789366196018718420E-15, 1.000000000000000000 ) ) ;
#184541=CARTESIAN_POINT ( 'NONE',  ( -16.93772744219066340, 66.00645889125951271, -90.42504551255468925 ) ) ;
#184575=CARTESIAN_POINT ( 'NONE',  ( 20.73486653747088582, 68.75000000001178080, -82.17310748452436542 ) ) ;
#184590=EDGE_CURVE ( 'NONE', #81650, #24606, #224644, .T. ) ;
#184700=CARTESIAN_POINT ( 'NONE',  ( -16.87683809663752399, 52.34166666667851331, -86.27310748452447342 ) ) ;
#184722=LINE ( 'NONE', #66068, #30624 ) ;
#185039=DIRECTION ( 'NONE',  ( -1.020425574104004196E-15, -6.982962677686266711E-15, 1.000000000000000000 ) ) ;
#185082=ADVANCED_FACE ( 'NONE', ( #230799 ), #169567, .F. ) ;
#185289=FACE_OUTER_BOUND ( 'NONE', #85333, .T. ) ;
#185328=ADVANCED_FACE ( 'NONE', ( #178534 ), #195530, .F. ) ;
#185674=ORIENTED_EDGE ( 'NONE', *, *, #188389, .T. ) ;
#185919=CARTESIAN_POINT ( 'NONE',  ( -18.40000000000000213, 64.66825945288661615, -82.17310748452439384 ) ) ;
#186104=B_SPLINE_CURVE_WITH_KNOTS ( 'NONE', 3,
 ( #124007, #144823, #43179, #202251, #224369, #143548, #45736, #147408, #106984, #2744 ),
 .UNSPECIFIED., .F., .F.,
 ( 4, 3, 3, 4 ),
 ( 7.632826238683052976E-06, 4.756916949876723342E-05, 9.484459048151396053E-05, 0.0001435500935099974268 ),
 .UNSPECIFIED. ) ;
#186135=DIRECTION ( 'NONE',  ( 0.7071067811865463515, 0.7071067811865487940, 4.937700262164540154E-15 ) ) ;
#186483=CARTESIAN_POINT ( 'NONE',  ( -20.65000000000000568, 68.75000000001188027, -90.37310748452435405 ) ) ;
#186898=VECTOR ( 'NONE', #136912, 1000.000000000000000 ) ;
#186938=CARTESIAN_POINT ( 'NONE',  ( -16.82542659449974565, 66.06550010858438782, -82.26774308455044604 ) ) ;
#186965=CARTESIAN_POINT ( 'NONE',  ( -16.80070461187855457, 66.05000000001085425, -90.37614365536641969 ) ) ;
#187302=CARTESIAN_POINT ( 'NONE',  ( -17.11825945287481687, 66.05000000001182059, -82.17310748452439384 ) ) ;
#187311=CARTESIAN_POINT ( 'NONE',  ( -21.65000000000000213, 68.75000000001182343, -82.17310748452436542 ) ) ;
#187470=CARTESIAN_POINT ( 'NONE',  ( -16.90987985657661241, 66.04219248183207469, -82.15382039564075001 ) ) ;
#187517=ORIENTED_EDGE ( 'NONE', *, *, #154310, .F. ) ;
#187836=AXIS2_PLACEMENT_3D ( 'NONE', #123393, #4700, #41315 ) ;
#187843=CARTESIAN_POINT ( 'NONE',  ( -16.87331047859651179, 66.05000000001187743, -90.37310748452438247 ) ) ;
#187970=DIRECTION ( 'NONE',  ( 0.000000000000000000, -6.982962677686266711E-15, 1.000000000000000000 ) ) ;
#187976=B_SPLINE_CURVE_WITH_KNOTS ( 'NONE', 3,
 ( #257482, #73800, #38506, #54195, #213268, #15091, #256187, #34667, #234119, #77593, #114177, #94605, #253675, #75086 ),
 .UNSPECIFIED., .F., .F.,
 ( 4, 2, 2, 2, 2, 2, 4 ),
 ( 0.000000000000000000, 2.389617747645373272E-05, 4.779235495290746544E-05, 9.558470990578175430E-05, 0.0001911694198114850666, 0.0003823388396228845354, 0.0007646776792456835272 ),
 .UNSPECIFIED. ) ;
#188141=LINE ( 'NONE', #143857, #210271 ) ;
#188175=SHAPE_REPRESENTATION_RELATIONSHIP ( 'NONE' , 'NONE' ,  #125202, #14150 ) ;
#188238=CARTESIAN_POINT ( 'NONE',  ( -16.95709691156456955, 66.05000000001189164, -90.36304992201408481 ) ) ;
#188389=EDGE_CURVE ( 'NONE', #256979, #179202, #252624, .T. ) ;
#188430=CARTESIAN_POINT ( 'NONE',  ( 20.09999999999999787, 66.25000000001185185, -90.37310748452436826 ) ) ;
#188498=CARTESIAN_POINT ( 'NONE',  ( 15.74999999999999645, 66.65000000001185754, -86.27310748452437394 ) ) ;
#188565=CARTESIAN_POINT ( 'NONE',  ( -17.05016517656045849, 66.05000000001182059, -82.19580548052314839 ) ) ;
#188747=ORIENTED_EDGE ( 'NONE', *, *, #95168, .T. ) ;
#188749=EDGE_CURVE ( 'NONE', #256979, #236175, #97797, .T. ) ;
#188886=AXIS2_PLACEMENT_3D ( 'NONE', #116239, #220469, #56221 ) ;
#188922=CARTESIAN_POINT ( 'NONE',  ( -18.40000000000000213, 64.25000000001182343, -82.17310748452439384 ) ) ;
#188949=ORIENTED_EDGE ( 'NONE', *, *, #19883, .F. ) ;
#189338=VERTEX_POINT ( 'NONE', #48128 ) ;
#189410=CARTESIAN_POINT ( 'NONE',  ( -16.87036670365549540, 66.01058118071020431, -90.50266760182644532 ) ) ;
#189439=CARTESIAN_POINT ( 'NONE',  ( 12.33938619321247643, 66.63927620602579793, -85.70918028991771109 ) ) ;
#189458=ORIENTED_EDGE ( 'NONE', *, *, #19572, .T. ) ;
#189460=SURFACE_STYLE_USAGE ( .BOTH. , #48645 ) ;
#189642=ORIENTED_EDGE ( 'NONE', *, *, #225891, .T. ) ;
#189813=CARTESIAN_POINT ( 'NONE',  ( -16.93589915522259304, 65.99137474131595127, -82.08254738256407279 ) ) ;
#189920=ORIENTED_EDGE ( 'NONE', *, *, #150279, .F. ) ;
#189925=MANIFOLD_SOLID_BREP ( 'Stock-MAS-200-1', #49362 ) ;
#190025=ORIENTED_EDGE ( 'NONE', *, *, #3416, .T. ) ;
#190644=AXIS2_PLACEMENT_3D ( 'NONE', #198033, #98907, #257965 ) ;
#190718=CARTESIAN_POINT ( 'NONE',  ( -17.22767730083219817, 65.65075578754462526, -91.66553617509441665 ) ) ;
#190840=CARTESIAN_POINT ( 'NONE',  ( -16.93388492042258164, 66.01145817749596745, -90.42365260771055091 ) ) ;
#191082=CARTESIAN_POINT ( 'NONE',  ( -18.40000000000000213, 64.52683809664932824, -82.13168612828711446 ) ) ;
#191092=ADVANCED_FACE ( 'NONE', ( #77123 ), #18437, .T. ) ;
#191115=CARTESIAN_POINT ( 'NONE',  ( -16.93658211146644987, 66.00589133767060446, -82.11881241456870839 ) ) ;
#191238=VERTEX_POINT ( 'NONE', #67835 ) ;
#191244=ORIENTED_EDGE ( 'NONE', *, *, #46253, .F. ) ;
#191511=B_SPLINE_CURVE_WITH_KNOTS ( 'NONE', 3,
 ( #204432, #6231, #85743, #59774, #139318, #199325, #20699, #179766, #1082, #220167, #187470, #111772, #11390 ),
 .UNSPECIFIED., .F., .F.,
 ( 4, 3, 3, 3, 4 ),
 ( -3.224855718275878119E-06, 0.000000000000000000, 6.199515528664636366E-06, 4.034952380127537373E-05, 7.452715123699773787E-05 ),
 .UNSPECIFIED. ) ;
#191771=CARTESIAN_POINT ( 'NONE',  ( -16.87683809663752399, 66.15000000001182912, -82.92547150272068279 ) ) ;
#191825=ADVANCED_FACE ( 'NONE', ( #231750 ), #53091, .F. ) ;
#192033=CARTESIAN_POINT ( 'NONE',  ( 12.25000000000000000, 66.15000000001185754, -86.27310748452437394 ) ) ;
#192076=CARTESIAN_POINT ( 'NONE',  ( -21.65000000000000213, 68.75000000001189449, -93.77310748452435973 ) ) ;
#192079=CARTESIAN_POINT ( 'NONE',  ( -16.92778301347301451, 65.99905508317638692, -90.45162559249260426 ) ) ;
#192356=CARTESIAN_POINT ( 'NONE',  ( 15.74999999999999289, 66.65000000001187175, -86.50453852712173841 ) ) ;
#192388=ORIENTED_EDGE ( 'NONE', *, *, #255105, .F. ) ;
#192647=ORIENTED_EDGE ( 'NONE', *, *, #203329, .T. ) ;
#192697=CARTESIAN_POINT ( 'NONE',  ( -16.87683809663752399, 66.15000000001182912, -82.92547150272068279 ) ) ;
#192703=CARTESIAN_POINT ( 'NONE',  ( -16.87665923198281348, 66.05000000001182059, -82.17310748452439384 ) ) ;
#192771=VECTOR ( 'NONE', #8190, 1000.000000000000000 ) ;
#192870=CARTESIAN_POINT ( 'NONE',  ( -17.71734398241074615, 65.15764277154733009, -92.74824573752999868 ) ) ;
#193009=ADVANCED_FACE ( 'NONE', ( #239495 ), #60831, .T. ) ;
#193128=ADVANCED_FACE ( 'NONE', ( #88078 ), #245911, .T. ) ;
#193295=CARTESIAN_POINT ( 'NONE',  ( 13.77030915526558630, 66.54399267394252604, -84.53447399037763432 ) ) ;
#193661=CARTESIAN_POINT ( 'NONE',  ( -16.93262454970419384, 65.99797953208144463, -82.09603125828706993 ) ) ;
#193790=DIRECTION ( 'NONE',  ( 0.000000000000000000, 0.000000000000000000, -1.000000000000000000 ) ) ;
#193997=CARTESIAN_POINT ( 'NONE',  ( -16.89208623190940273, 66.04842205103632580, -82.16783528130611103 ) ) ;
#194271=CARTESIAN_POINT ( 'NONE',  ( -12.60206096961791999, 66.61031399435616152, -87.35026397817303234 ) ) ;
#194625=EDGE_CURVE ( 'NONE', #54224, #179202, #29807, .T. ) ;
#194646=DIRECTION ( 'NONE',  ( -1.000000000000000000, 0.000000000000000000, 0.000000000000000000 ) ) ;
#194899=( BOUNDED_SURFACE ( )  B_SPLINE_SURFACE ( 3, 2, ( 
 ( #95815, #175408, #254851 ),
 ( #76265, #155837, #197498 ),
 ( #18863, #38434, #196217 ),
 ( #235337, #198783, #136216 ),
 ( #179255, #215769, #177960 ),
 ( #37171, #17571, #257418 ),
 ( #78820, #158417, #237913 ),
 ( #20168, #224761, #87808 ),
 ( #241762, #186965, #166129 ),
 ( #46131, #164810, #203925 ) ),
 .UNSPECIFIED., .F., .F., .F. ) 
 B_SPLINE_SURFACE_WITH_KNOTS ( ( 4, 2, 2, 2, 4 ),
 ( 3, 3 ),
 ( 0.002161241639767785133, 0.002579950749617447234, 0.002789305304542278284, 0.002893982582004694243, 0.002998659859467109768 ),
 ( 0.000000000000000000, 1.000000000000000000 ),
 .UNSPECIFIED. ) 
 GEOMETRIC_REPRESENTATION_ITEM ( )  RATIONAL_B_SPLINE_SURFACE ( (
 ( 1.000000000000000000, 0.7071067811864985009, 1.000000000000000000),
 ( 1.000000000000000000, 0.7632447400663817660, 1.000000000000000000),
 ( 1.000000000000000000, 0.8158073005109720555, 1.000000000000000000),
 ( 1.000000000000000000, 0.8906973462395535446, 1.000000000000000000),
 ( 1.000000000000000000, 0.9149408947797941227, 1.000000000000000000),
 ( 1.000000000000000000, 0.9493368785276861122, 1.000000000000000000),
 ( 1.000000000000000000, 0.9605194247156072507, 1.000000000000000000),
 ( 1.000000000000000000, 0.9803630264781721948, 1.000000000000000000),
 ( 1.000000000000000000, 0.9900844824270734756, 1.000000000000000000),
 ( 1.000000000000000000, 0.9894588281429241849, 1.000000000000000000) ) ) 
 REPRESENTATION_ITEM ( '' )  SURFACE ( )  );
#194915=AXIS2_PLACEMENT_3D ( 'NONE', #115265, #18732, #96946 ) ;
#194960=CARTESIAN_POINT ( 'NONE',  ( -16.93433913041102912, 65.99402157848787454, -82.08774205712920491 ) ) ;
#195004=PLANE ( 'NONE',  #29866 ) ;
#195022=DIRECTION ( 'NONE',  ( -1.000000000000000000, 0.000000000000000000, 0.000000000000000000 ) ) ;
#195143=CARTESIAN_POINT ( 'NONE',  ( -18.40000000000000213, 64.25000000001179501, -78.77310748452440237 ) ) ;
#195530=PLANE ( 'NONE',  #238932 ) ;
#195663=LINE ( 'NONE', #177390, #58964 ) ;
#195719=CARTESIAN_POINT ( 'NONE',  ( 18.54999999999999716, 67.25000000001178080, -82.17310748452437963 ) ) ;
#195759=VECTOR ( 'NONE', #215998, 1000.000000000000000 ) ;
#196034=B_SPLINE_CURVE_WITH_KNOTS ( 'NONE', 3,
 ( #252307, #232781, #213185, #129805, #151971, #54114, #209339, #231494, #9859, #133660, #11151, #248479, #30740, #34582, #253591, #94520, #75001, #249761, #230191, #69860, #214470, #110238, #170272, #35865, #192356, #188498 ),
 .UNSPECIFIED., .F., .F.,
 ( 4, 2, 2, 2, 2, 2, 2, 2, 2, 2, 2, 2, 4 ),
 ( 0.005476422646581347378, 0.006160811967703556588, 0.006845201288825765798, 0.007187395949386870403, 0.007529590609947975008, 0.007871785270509079613, 0.008213979931070184218, 0.008556174591631288823, 0.008898369252192393428, 0.009240563912753498033, 0.009582758573314602638, 0.01026714789443681185, 0.01095153721555902106 ),
 .UNSPECIFIED. ) ;
#196087=CARTESIAN_POINT ( 'NONE',  ( -16.89268316805466341, 66.04827818676967865, -90.37885996306994230 ) ) ;
#196217=CARTESIAN_POINT ( 'NONE',  ( -16.87333278164142669, 66.11739021543297667, -89.88993967837170374 ) ) ;
#196250=EDGE_CURVE ( 'NONE', #77215, #14013, #144274, .T. ) ;
#196362=( BOUNDED_CURVE ( )  B_SPLINE_CURVE ( 3, ( #95954, #94674, #136342, #213332 ),
 .UNSPECIFIED., .F., .F. ) 
 B_SPLINE_CURVE_WITH_KNOTS ( ( 4, 4 ),
 ( 2.589852378279006828, 2.850972632318389710 ),
 .UNSPECIFIED. ) 
 CURVE ( )  GEOMETRIC_REPRESENTATION_ITEM ( )  RATIONAL_B_SPLINE_CURVE ( ( 1.000000000000000000, 0.9943260843901262636, 0.9943260843901262636, 1.000000000000000000 ) ) 
 REPRESENTATION_ITEM ( '' )  );
#196422=CARTESIAN_POINT ( 'NONE',  ( 18.54999999999999716, 67.25000000001185185, -90.37310748452436826 ) ) ;
#196755=ORIENTED_EDGE ( 'NONE', *, *, #135287, .T. ) ;
#196836=EDGE_LOOP ( 'NONE', ( #43216, #96348, #209756, #21967 ) ) ;
#196989=FACE_OUTER_BOUND ( 'NONE', #110392, .T. ) ;
#197354=CARTESIAN_POINT ( 'NONE',  ( -16.92132318717937522, 66.03392997600593617, -90.40070085417231383 ) ) ;
#197498=CARTESIAN_POINT ( 'NONE',  ( -16.87683809663752754, 66.13411015068085419, -89.75568067745427925 ) ) ;
#197541=CARTESIAN_POINT ( 'NONE',  ( -16.94445028196808778, 66.00793639031412852, -90.41577730610593733 ) ) ;
#197553=LINE ( 'NONE', #118020, #29987 ) ;
#197731=CARTESIAN_POINT ( 'NONE',  ( -18.40000000000000213, 64.25000000001188027, -90.37310748452439668 ) ) ;
#197810=VERTEX_POINT ( 'NONE', #95618 ) ;
#197903=ORIENTED_EDGE ( 'NONE', *, *, #149436, .T. ) ;
#197934=PLANE ( 'NONE',  #206148 ) ;
#197966=CARTESIAN_POINT ( 'NONE',  ( -33.72168855820452649, 64.52683809664929981, -78.77310748452438816 ) ) ;
#198033=CARTESIAN_POINT ( 'NONE',  ( -23.25000000000000355, 70.35000000001190301, -93.77310748452434552 ) ) ;
#198061=CARTESIAN_POINT ( 'NONE',  ( 16.27683809663749770, 66.65000000001191438, -93.77310748452437394 ) ) ;
#198191=CYLINDRICAL_SURFACE ( 'NONE', #93351, 0.9000000000000014655 ) ;
#198783=CARTESIAN_POINT ( 'NONE',  ( -16.88705144915409662, 66.05000000001187743, -90.09212888981180356 ) ) ;
#198840=DIRECTION ( 'NONE',  ( -1.000000000000000000, 0.000000000000000000, -0.000000000000000000 ) ) ;
#199035=CARTESIAN_POINT ( 'NONE',  ( -15.15564720441980739, 66.58929125296474183, -84.95389907868026569 ) ) ;
#199071=ORIENTED_EDGE ( 'NONE', *, *, #12597, .T. ) ;
#199269=LINE ( 'NONE', #197966, #125869 ) ;
#199325=CARTESIAN_POINT ( 'NONE',  ( -16.94052228080551714, 66.01372026691295503, -82.13273198185495971 ) ) ;
#199377=CARTESIAN_POINT ( 'NONE',  ( -16.88815647973234135, 66.04916738069613302, -90.37589042119837757 ) ) ;
#199398=CARTESIAN_POINT ( 'NONE',  ( -13.43673303185029333, 66.55335100938299320, -87.93394418860120254 ) ) ;
#199659=DIRECTION ( 'NONE',  ( -1.000000000000000000, 0.000000000000000000, 0.000000000000000000 ) ) ;
#199674=CIRCLE ( 'NONE', #83077, 0.1000000000000028644 ) ;
#199875=FILL_AREA_STYLE_COLOUR ( '', #215377 ) ;
#200141=EDGE_CURVE ( 'NONE', #14757, #117904, #11228, .T. ) ;
#200147=CARTESIAN_POINT ( 'NONE',  ( -18.40000000000000213, 64.25000000001188027, -90.37310748452439668 ) ) ;
#200271=CARTESIAN_POINT ( 'NONE',  ( -16.93440969289731157, 66.00481482419790780, -90.43187329951359743 ) ) ;
#200298=DIRECTION ( 'NONE',  ( -0.000000000000000000, -6.982962677686266711E-15, 1.000000000000000000 ) ) ;
#200313=VERTEX_POINT ( 'NONE', #116739 ) ;
#200368=ORIENTED_EDGE ( 'NONE', *, *, #4704, .F. ) ;
#200690=CARTESIAN_POINT ( 'NONE',  ( -16.77977881697927032, 66.05339806647896239, -90.36172891140932961 ) ) ;
#200763=CARTESIAN_POINT ( 'NONE',  ( 20.99999999999999645, 66.25000000001190870, -93.77310748452438816 ) ) ;
#200810=AXIS2_PLACEMENT_3D ( 'NONE', #201025, #100593, #156785 ) ;
#201025=CARTESIAN_POINT ( 'NONE',  ( -21.64999999999999858, 65.95000000001181206, -82.27310748452437394 ) ) ;
#201088=CARTESIAN_POINT ( 'NONE',  ( 23.24999999999999645, 67.17743825834540417, -82.17310748452437963 ) ) ;
#201180=CARTESIAN_POINT ( 'NONE',  ( -15.75000000000000355, 66.65000000001185754, -86.27310748452437394 ) ) ;
#201259=AXIS2_PLACEMENT_3D ( 'NONE', #6754, #229658, #187970 ) ;
#201406=VERTEX_POINT ( 'NONE', #74825 ) ;
#201587=CARTESIAN_POINT ( 'NONE',  ( -15.73854595235691889, 66.64858632091043944, -86.04276391697541726 ) ) ;
#201655=AXIS2_PLACEMENT_3D ( 'NONE', #184700, #221250, #124746 ) ;
#201796=ORIENTED_EDGE ( 'NONE', *, *, #250997, .F. ) ;
#201874=FACE_OUTER_BOUND ( 'NONE', #179844, .T. ) ;
#202204=VERTEX_POINT ( 'NONE', #167936 ) ;
#202251=CARTESIAN_POINT ( 'NONE',  ( -16.87304349924914604, 66.03825492205463377, -82.13404080947913144 ) ) ;
#202521=CARTESIAN_POINT ( 'NONE',  ( -16.94107738177414291, 65.98576071487519812, -82.07310748452438531 ) ) ;
#202542=ORIENTED_EDGE ( 'NONE', *, *, #173852, .F. ) ;
#202925=AXIS2_PLACEMENT_3D ( 'NONE', #207496, #182797, #206193 ) ;
#202972=CARTESIAN_POINT ( 'NONE',  ( -16.87683809663752399, 66.15000000001188596, -90.37310748452438247 ) ) ;
#203036=EDGE_LOOP ( 'NONE', ( #18956, #42476 ) ) ;
#203154=DIRECTION ( 'NONE',  ( 1.186688945009010077E-16, 1.000000000000000000, 6.982962677686266711E-15 ) ) ;
#203329=EDGE_CURVE ( 'NONE', #7257, #103638, #181662, .T. ) ;
#203401=AXIS2_PLACEMENT_3D ( 'NONE', #221913, #129267, #45871 ) ;
#203443=CARTESIAN_POINT ( 'NONE',  ( -18.39418127959864790, 64.51609439831364057, -78.77310748452438816 ) ) ;
#203500=EDGE_LOOP ( 'NONE', ( #257324, #62960, #21628, #22387 ) ) ;
#203516=DIRECTION ( 'NONE',  ( 0.000000000000000000, 6.982962677686266711E-15, -1.000000000000000000 ) ) ;
#203588=CARTESIAN_POINT ( 'NONE',  ( -16.80100914604134132, 66.05685090590822028, -82.20606335723671521 ) ) ;
#203606=CIRCLE ( 'NONE', #78688, 0.9000000000000014655 ) ;
#203647=CARTESIAN_POINT ( 'NONE',  ( -18.40000000000000213, 64.51332499825412015, -78.77310748452438816 ) ) ;
#203709=SURFACE_SIDE_STYLE ('',( #101999 ) ) ;
#203711=ORIENTED_EDGE ( 'NONE', *, *, #169881, .T. ) ;
#203761=EDGE_LOOP ( 'NONE', ( #110354, #202542, #171437, #19755 ) ) ;
#203925=CARTESIAN_POINT ( 'NONE',  ( -16.77431908686106610, 66.05419424549388907, -90.35894670217462021 ) ) ;
#204006=FACE_OUTER_BOUND ( 'NONE', #233884, .T. ) ;
#204264=CARTESIAN_POINT ( 'NONE',  ( -16.95709691156445587, 66.05000000001182059, -82.18316504703474834 ) ) ;
#204432=CARTESIAN_POINT ( 'NONE',  ( -16.94445028196807002, 66.00793639031407167, -82.13043766294282477 ) ) ;
#204543=EDGE_CURVE ( 'NONE', #253194, #179449, #199674, .T. ) ;
#204593=PLANE ( 'NONE',  #589 ) ;
#204667=ORIENTED_EDGE ( 'NONE', *, *, #208611, .T. ) ;
#204773=ORIENTED_EDGE ( 'NONE', *, *, #46531, .F. ) ;
#204986=ORIENTED_EDGE ( 'NONE', *, *, #123244, .T. ) ;
#205408=VERTEX_POINT ( 'NONE', #140083 ) ;
#205465=CARTESIAN_POINT ( 'NONE',  ( 13.99999999999999822, 66.15000000001185754, -86.27310748452437394 ) ) ;
#205773=VERTEX_POINT ( 'NONE', #236333 ) ;
#206118=CARTESIAN_POINT ( 'NONE',  ( -18.40000000000000213, 64.51332499825421962, -93.77310748452438816 ) ) ;
#206148=AXIS2_PLACEMENT_3D ( 'NONE', #36328, #115847, #134105 ) ;
#206193=DIRECTION ( 'NONE',  ( 1.000000000000000000, 0.000000000000000000, 0.000000000000000000 ) ) ;
#206354=ADVANCED_FACE ( 'NONE', ( #220330 ), #204593, .F. ) ;
#206463=ADVANCED_FACE ( 'NONE', ( #128929 ), #195004, .F. ) ;
#206474=CARTESIAN_POINT ( 'NONE',  ( -16.85722902420155478, 66.05000000001183480, -82.28865495829489873 ) ) ;
#206850=CARTESIAN_POINT ( 'NONE',  ( -16.92209698673680052, 66.05000000001182059, -82.23374305157656750 ) ) ;
#206862=ORIENTED_EDGE ( 'NONE', *, *, #15470, .T. ) ;
#207281=ORIENTED_EDGE ( 'NONE', *, *, #214199, .F. ) ;
#207496=CARTESIAN_POINT ( 'NONE',  ( 13.99999999999999822, 66.15000000001185754, -86.27310748452437394 ) ) ;
#207609=ORIENTED_EDGE ( 'NONE', *, *, #2228, .T. ) ;
#207758=CARTESIAN_POINT ( 'NONE',  ( -16.79363873026997922, 66.05114977059336923, -82.17695370307890812 ) ) ;
#207781=CARTESIAN_POINT ( 'NONE',  ( -16.92280123533721792, 66.05000000001182059, -82.37373979860946349 ) ) ;
#207843=LINE ( 'NONE', #103549, #139313 ) ;
#208074=CARTESIAN_POINT ( 'NONE',  ( -16.87036670365548474, 65.91505003675652574, -82.07310748452438531 ) ) ;
#208287=CARTESIAN_POINT ( 'NONE',  ( -16.87683809663752399, 66.15000000001187175, -89.62074346632807931 ) ) ;
#208386=DIRECTION ( 'NONE',  ( -1.000000000000000000, 0.000000000000000000, 0.000000000000000000 ) ) ;
#208611=EDGE_CURVE ( 'NONE', #65335, #98906, #85061, .T. ) ;
#208693=ORIENTED_EDGE ( 'NONE', *, *, #200141, .F. ) ;
#208962=CARTESIAN_POINT ( 'NONE',  ( -16.91256925476571027, 66.01426884188369115, -90.49074997352965966 ) ) ;
#208989=CARTESIAN_POINT ( 'NONE',  ( 15.73863059295127798, 66.64859682587018597, -86.04357704768588633 ) ) ;
#209015=( LENGTH_UNIT ( ) NAMED_UNIT ( * ) SI_UNIT ( .MILLI., .METRE. ) );
#209041=CARTESIAN_POINT ( 'NONE',  ( -16.87401514999234209, 66.05000000001182059, -82.24308949199205188 ) ) ;
#209332=CARTESIAN_POINT ( 'NONE',  ( 20.04999999999999716, 67.25000000001186606, -93.77310748452437394 ) ) ;
#209339=CARTESIAN_POINT ( 'NONE',  ( 12.93225390519045170, 66.58234804117083172, -87.66432009208394049 ) ) ;
#209419=CARTESIAN_POINT ( 'NONE',  ( 20.73486653747088937, 68.25000000001185185, -93.77310748452435973 ) ) ;
#209586=ORIENTED_EDGE ( 'NONE', *, *, #86502, .T. ) ;
#209659=VERTEX_POINT ( 'NONE', #139693 ) ;
#209756=ORIENTED_EDGE ( 'NONE', *, *, #150279, .T. ) ;
#209788=EDGE_CURVE ( 'NONE', #225448, #17815, #85965, .T. ) ;
#210142=CARTESIAN_POINT ( 'NONE',  ( 23.24999999999999645, 64.25000000001182343, -82.17310748452440805 ) ) ;
#210271=VECTOR ( 'NONE', #147733, 1000.000000000000000 ) ;
#210360=AXIS2_PLACEMENT_3D ( 'NONE', #91752, #252101, #171342 ) ;
#210378=FACE_OUTER_BOUND ( 'NONE', #102642, .T. ) ;
#210651=CARTESIAN_POINT ( 'NONE',  ( -16.93211319090181632, 66.00001321885433470, -82.10060198525131625 ) ) ;
#210966=EDGE_CURVE ( 'NONE', #10053, #189338, #147378, .T. ) ;
#211001=CARTESIAN_POINT ( 'NONE',  ( -23.25000000000000355, 64.25000000001179501, -78.77310748452440237 ) ) ;
#211058=LINE ( 'NONE', #70294, #74769 ) ;
#211314=EDGE_CURVE ( 'NONE', #34828, #153574, #75790, .T. ) ;
#211451=EDGE_CURVE ( 'NONE', #177874, #86629, #239530, .T. ) ;
#211590=PLANE ( 'NONE',  #217808 ) ;
#211820=B_SPLINE_CURVE_WITH_KNOTS ( 'NONE', 3,
 ( #241071, #119846, #199377, #239775, #61127, #220217, #62423, #141944, #66272, #68851 ),
 .UNSPECIFIED., .F., .F.,
 ( 4, 3, 3, 4 ),
 ( 1.957469226477651626E-15, 8.145022132840017156E-06, 1.905645951092857371E-05, 2.061107371226198839E-05 ),
 .UNSPECIFIED. ) ;
#211977=VERTEX_POINT ( 'NONE', #41879 ) ;
#212008=AXIS2_PLACEMENT_3D ( 'NONE', #123094, #104765, #184325 ) ;
#212090=EDGE_LOOP ( 'NONE', ( #161125, #57972, #173965, #32607, #172867, #33130, #100193, #143012, #90728, #5756, #118408, #30107, #117836, #241858, #203711, #233900, #154608, #114569 ) ) ;
#212102=ORIENTED_EDGE ( 'NONE', *, *, #244962, .T. ) ;
#212853=CARTESIAN_POINT ( 'NONE',  ( 14.88075390448864788, 66.56831044948773979, -84.74381745228832585 ) ) ;
#212911=CARTESIAN_POINT ( 'NONE',  ( -16.92570016628985385, 66.04121104227199623, -90.40245681448537596 ) ) ;
#212933=CARTESIAN_POINT ( 'NONE',  ( -16.94107738177415712, 65.98576071487524075, -90.47310748452437679 ) ) ;
#212940=CARTESIAN_POINT ( 'NONE',  ( -17.11825945287482753, 65.95000000001188312, -90.37310748452436826 ) ) ;
#213098=DIRECTION ( 'NONE',  ( -0.7071067811865463515, -0.7071067811865487940, -4.937700262164540154E-15 ) ) ;
#213132=CARTESIAN_POINT ( 'NONE',  ( -21.64999999999999858, 66.65000000001188596, -90.37310748452436826 ) ) ;
#213185=CARTESIAN_POINT ( 'NONE',  ( 12.29592348164039528, 66.64419340838171024, -86.73200495297822954 ) ) ;
#213268=CARTESIAN_POINT ( 'NONE',  ( -16.80468759584937288, 66.05784632487771546, -90.33308861832274772 ) ) ;
#213332=CARTESIAN_POINT ( 'NONE',  ( 16.87683809663750267, 66.05000000001187743, -90.37310748452438247 ) ) ;
#213376=VECTOR ( 'NONE', #117119, 1000.000000000000000 ) ;
#213802=CARTESIAN_POINT ( 'NONE',  ( -13.54795643572457919, 66.54933111084433506, -87.96756099431704001 ) ) ;
#213937=EDGE_CURVE ( 'NONE', #7257, #66229, #43714, .T. ) ;
#214004=ORIENTED_EDGE ( 'NONE', *, *, #246309, .T. ) ;
#214137=CIRCLE ( 'NONE', #201655, 14.20833333333333748 ) ;
#214199=EDGE_CURVE ( 'NONE', #91289, #10718, #34459, .T. ) ;
#214402=DIRECTION ( 'NONE',  ( 0.5932847527679310229, 0.8049926720990042694, 6.257843056355992909E-15 ) ) ;
#214437=ORIENTED_EDGE ( 'NONE', *, *, #61458, .T. ) ;
#214470=CARTESIAN_POINT ( 'NONE',  ( 15.15590539855245744, 66.58931770574392317, -87.59196404257609458 ) ) ;
#214548=CARTESIAN_POINT ( 'NONE',  ( 20.73486653747090003, 68.75000000001178080, -82.17310748452436542 ) ) ;
#215021=EDGE_LOOP ( 'NONE', ( #189920, #165465, #21208, #239181 ) ) ;
#215091=VERTEX_POINT ( 'NONE', #157655 ) ;
#215214=DIRECTION ( 'NONE',  ( 0.000000000000000000, 1.000000000000000000, 6.982962677686266711E-15 ) ) ;
#215222=ORIENTED_EDGE ( 'NONE', *, *, #176310, .F. ) ;
#215354=ORIENTED_EDGE ( 'NONE', *, *, #88142, .F. ) ;
#215377=COLOUR_RGB ( '', 0.72549020, 0.75294118, 0.79215686) ;
#215384=AXIS2_PLACEMENT_3D ( 'NONE', #109850, #229808, #173750 ) ;
#215769=CARTESIAN_POINT ( 'NONE',  ( -16.87998658237743399, 66.05000000001187743, -90.15946791678636885 ) ) ;
#215828=ORIENTED_EDGE ( 'NONE', *, *, #46253, .T. ) ;
#215951=ADVANCED_FACE ( 'NONE', ( #100126 ), #178442, .F. ) ;
#215998=DIRECTION ( 'NONE',  ( -1.000000000000000000, 0.000000000000000000, -0.000000000000000000 ) ) ;
#216038=EDGE_CURVE ( 'NONE', #139587, #257124, #2319, .T. ) ;
#216332=ADVANCED_FACE ( 'NONE', ( #43724 ), #2007, .F. ) ;
#216524=EDGE_CURVE ( 'NONE', #153515, #14757, #34789, .T. ) ;
#216749=CARTESIAN_POINT ( 'NONE',  ( -16.89318236219977010, 66.04846474213672991, -90.37823711663024540 ) ) ;
#216777=VERTEX_POINT ( 'NONE', #26115 ) ;
#216918=DIRECTION ( 'NONE',  ( 1.000000000000000000, 0.000000000000000000, 0.000000000000000000 ) ) ;
#216958=CARTESIAN_POINT ( 'NONE',  ( -21.65000000000000213, 66.05000000001187743, -90.37310748452438247 ) ) ;
#217118=ORIENTED_EDGE ( 'NONE', *, *, #141397, .T. ) ;
#217238=CARTESIAN_POINT ( 'NONE',  ( 20.27550659511089037, 66.78395627750296626, -82.17310748452437963 ) ) ;
#217324=VERTEX_POINT ( 'NONE', #156034 ) ;
#217581=FACE_OUTER_BOUND ( 'NONE', #138823, .T. ) ;
#217650=DIRECTION ( 'NONE',  ( 1.000000000000000000, -0.000000000000000000, 0.000000000000000000 ) ) ;
#217792=CARTESIAN_POINT ( 'NONE',  ( -16.89268316805465986, 66.04827818676963602, -82.16735500597883401 ) ) ;
#217805=ORIENTED_EDGE ( 'NONE', *, *, #241570, .F. ) ;
#217808=AXIS2_PLACEMENT_3D ( 'NONE', #205465, #26872, #32994 ) ;
#217867=ORIENTED_EDGE ( 'NONE', *, *, #238325, .T. ) ;
#217950=CARTESIAN_POINT ( 'NONE',  ( -18.40000000000000213, 64.51332499825421962, -93.77310748452438816 ) ) ;
#218071=CARTESIAN_POINT ( 'NONE',  ( -16.87036670365549895, 66.01058118071021852, -90.50266760182643111 ) ) ;
#218507=AXIS2_PLACEMENT_3D ( 'NONE', #209419, #251100, #195022 ) ;
#218567=CARTESIAN_POINT ( 'NONE',  ( -20.65000000000000568, 70.35000000001190301, -93.77310748452434552 ) ) ;
#218573=CARTESIAN_POINT ( 'NONE',  ( -12.68215100488890279, 66.60336962369413527, -85.11605009170608582 ) ) ;
#218818=CARTESIAN_POINT ( 'NONE',  ( 15.48841904831874849, 67.43841904833064405, -90.37310748452436826 ) ) ;
#218921=CARTESIAN_POINT ( 'NONE',  ( -14.56556274378147009, 66.55344247693928139, -87.93316553017845649 ) ) ;
#219028=CARTESIAN_POINT ( 'NONE',  ( 18.39999999999999503, 70.35000000001180354, -78.77310748452434552 ) ) ;
#219085=CARTESIAN_POINT ( 'NONE',  ( -23.25000000000000355, 64.25000000001190870, -93.77310748452438816 ) ) ;
#219415=CARTESIAN_POINT ( 'NONE',  ( 22.88900146558018989, 67.29609520889904672, -90.37310748452436826 ) ) ;
#219459=( GEOMETRIC_REPRESENTATION_CONTEXT ( 3 ) GLOBAL_UNCERTAINTY_ASSIGNED_CONTEXT ( ( #152071 ) ) GLOBAL_UNIT_ASSIGNED_CONTEXT ( ( #358, #103297, #79873 ) ) REPRESENTATION_CONTEXT ( 'NONE', 'WORKASPACE' ) );
#219550=CARTESIAN_POINT ( 'NONE',  ( -16.91256925476570672, 66.01426884188362010, -82.05546499551910244 ) ) ;
#219601=CARTESIAN_POINT ( 'NONE',  ( -16.85697194749126027, 66.09145628588818511, -82.45811175213816568 ) ) ;
#219872=VECTOR ( 'NONE', #135931, 1000.000000000000000 ) ;
#219926=ORIENTED_EDGE ( 'NONE', *, *, #7805, .F. ) ;
#219945=ORIENTED_EDGE ( 'NONE', *, *, #106507, .F. ) ;
#219979=( BOUNDED_CURVE ( )  B_SPLINE_CURVE ( 3, ( #61103, #97638, #160238, #41573 ),
 .UNSPECIFIED., .F., .F. ) 
 B_SPLINE_CURVE_WITH_KNOTS ( ( 4, 4 ),
 ( 1.570796326794908992, 2.617993877991481533 ),
 .UNSPECIFIED. ) 
 CURVE ( )  GEOMETRIC_REPRESENTATION_ITEM ( )  RATIONAL_B_SPLINE_CURVE ( ( 1.000000000000000000, 0.9106836025229633202, 0.9106836025229633202, 1.000000000000000000 ) ) 
 REPRESENTATION_ITEM ( '' )  );
#220167=CARTESIAN_POINT ( 'NONE',  ( -16.91776028072577631, 66.03659960638205462, -82.14808346982226794 ) ) ;
#220217=CARTESIAN_POINT ( 'NONE',  ( -16.87851181299898684, 66.04995707600411947, -90.37325099989129740 ) ) ;
#220330=FACE_OUTER_BOUND ( 'NONE', #164306, .T. ) ;
#220469=DIRECTION ( 'NONE',  ( -1.073024830501117725E-15, 6.982962677686266711E-15, -1.000000000000000000 ) ) ;
#220712=CARTESIAN_POINT ( 'NONE',  ( 18.39999999999997371, 64.25000000001190870, -93.77310748452438816 ) ) ;
#220841=CARTESIAN_POINT ( 'NONE',  ( -17.73285935859622953, 65.14201819621573009, -79.76454567473506074 ) ) ;
#220886=CARTESIAN_POINT ( 'NONE',  ( -16.89935556175729303, 66.05000000001182059, -82.66278384740907370 ) ) ;
#220925=ORIENTED_EDGE ( 'NONE', *, *, #238222, .F. ) ;
#221100=CARTESIAN_POINT ( 'NONE',  ( -16.94107738177415712, 65.98576071487524075, -90.47310748452437679 ) ) ;
#221250=DIRECTION ( 'NONE',  ( -1.000000000000000000, 1.186688945009010077E-16, 8.286604613020808509E-31 ) ) ;
#221662=CARTESIAN_POINT ( 'NONE',  ( -17.11825945287482753, 66.05000000001187743, -90.27310748452438816 ) ) ;
#221740=ORIENTED_EDGE ( 'NONE', *, *, #157873, .T. ) ;
#221913=CARTESIAN_POINT ( 'NONE',  ( 23.24999999999999645, 64.25000000001190870, -93.77310748452438816 ) ) ;
#221971=LINE ( 'NONE', #43373, #134972 ) ;
#222030=CARTESIAN_POINT ( 'NONE',  ( -16.94389599338511943, 66.00880201025681515, -90.41546268271413567 ) ) ;
#222130=CARTESIAN_POINT ( 'NONE',  ( -16.77732147262506146, 66.05403306739317770, -82.18661624124851528 ) ) ;
#222150=CYLINDRICAL_SURFACE ( 'NONE', #212008, 14.30833333333333890 ) ;
#222247=ORIENTED_EDGE ( 'NONE', *, *, #256860, .F. ) ;
#222516=DIRECTION ( 'NONE',  ( 0.000000000000000000, -6.982962677686266711E-15, 1.000000000000000000 ) ) ;
#222794=CARTESIAN_POINT ( 'NONE',  ( -16.80438519320023616, 66.05022090354351860, -90.37236920360311387 ) ) ;
#222870=EDGE_LOOP ( 'NONE', ( #175964, #236741, #171422, #100167 ) ) ;
#222880=FACE_OUTER_BOUND ( 'NONE', #241745, .T. ) ;
#222884=CARTESIAN_POINT ( 'NONE',  ( 13.99999999999999822, 66.15000000001185754, -86.27310748452437394 ) ) ;
#223236=ORIENTED_EDGE ( 'NONE', *, *, #75687, .T. ) ;
#223662=CARTESIAN_POINT ( 'NONE',  ( -16.94445028196808778, 66.00793639031412852, -90.41577730610593733 ) ) ;
#224072=ORIENTED_EDGE ( 'NONE', *, *, #142115, .T. ) ;
#224274=CARTESIAN_POINT ( 'NONE',  ( -18.34374000495059676, 64.52683809664929981, -78.77310748452438816 ) ) ;
#224302=AXIS2_PLACEMENT_3D ( 'NONE', #114969, #75846, #36756 ) ;
#224369=CARTESIAN_POINT ( 'NONE',  ( -16.86733706339143524, 66.03400947037214053, -82.11999218252567800 ) ) ;
#224566=DIRECTION ( 'NONE',  ( 0.000000000000000000, 1.000000000000000000, 6.982962677686266711E-15 ) ) ;
#224644=LINE ( 'NONE', #125554, #192771 ) ;
#224671=CARTESIAN_POINT ( 'NONE',  ( 20.99999999999999645, 66.25000000001182343, -82.17310748452439384 ) ) ;
#224688=CARTESIAN_POINT ( 'NONE',  ( -17.78241384940471193, 65.14442424718357927, -79.77214515698624098 ) ) ;
#224696=CARTESIAN_POINT ( 'NONE',  ( -23.25000000000000355, 70.35000000001190301, -93.77310748452434552 ) ) ;
#224761=CARTESIAN_POINT ( 'NONE',  ( -16.82055514392384055, 66.05000000001189164, -90.34630940998262361 ) ) ;
#224868=DIRECTION ( 'NONE',  ( 1.186688945009009831E-16, 1.000000000000000000, 6.982962677686266711E-15 ) ) ;
#225037=CARTESIAN_POINT ( 'NONE',  ( -18.40000000000000213, 64.58541674041208580, -90.37310748452436826 ) ) ;
#225101=FACE_OUTER_BOUND ( 'NONE', #157053, .T. ) ;
#225241=EDGE_LOOP ( 'NONE', ( #131704, #257256, #44101, #47605, #240978 ) ) ;
#225448=VERTEX_POINT ( 'NONE', #23624 ) ;
#225608=APPLICATION_CONTEXT ( 'automotive_design' ) ;
#225758=CARTESIAN_POINT ( 'NONE',  ( 23.04999999999999716, 67.17743825834548943, -93.77310748452437394 ) ) ;
#225769=EDGE_LOOP ( 'NONE', ( #6710, #167116 ) ) ;
#225778=PLANE ( 'NONE',  #201259 ) ;
#225891=EDGE_CURVE ( 'NONE', #225448, #169411, #171802, .T. ) ;
#225998=CARTESIAN_POINT ( 'NONE',  ( -16.77308656112214535, 66.05000000001183480, -82.17330067622667400 ) ) ;
#226053=ORIENTED_EDGE ( 'NONE', *, *, #213937, .T. ) ;
#226098=CARTESIAN_POINT ( 'NONE',  ( -23.25000000000000355, 64.25000000001188027, -90.37310748452439668 ) ) ;
#226288=CIRCLE ( 'NONE', #38895, 0.1999999999999987899 ) ;
#226338=CARTESIAN_POINT ( 'NONE',  ( -23.25000000000000355, 65.95000000001181206, -82.27310748452437394 ) ) ;
#226385=CARTESIAN_POINT ( 'NONE',  ( -17.11825945287481687, 65.95000000001181206, -82.17310748452439384 ) ) ;
#226590=DIRECTION ( 'NONE',  ( 0.000000000000000000, -1.000000000000000000, -6.982962677686266711E-15 ) ) ;
#226592=ORIENTED_EDGE ( 'NONE', *, *, #25918, .T. ) ;
#226846=CARTESIAN_POINT ( 'NONE',  ( -18.36973785203555920, 64.52449679952756867, -78.77310748452438816 ) ) ;
#226910=ADVANCED_FACE ( 'NONE', ( #196989 ), #18370, .F. ) ;
#226955=CARTESIAN_POINT ( 'NONE',  ( -16.84421487269769813, 66.05000000001187743, -90.35360536207943483 ) ) ;
#227144=EDGE_LOOP ( 'NONE', ( #91915, #7057, #204667, #147314 ) ) ;
#227262=CARTESIAN_POINT ( 'NONE',  ( 15.39170923737819763, 66.61047060254509233, -85.20599957163069860 ) ) ;
#227285=SURFACE_STYLE_FILL_AREA ( #164756 ) ;
#227577=VECTOR ( 'NONE', #60805, 999.9999999999998863 ) ;
#227637=DIRECTION ( 'NONE',  ( 0.000000000000000000, 0.000000000000000000, -1.000000000000000000 ) ) ;
#228224=DIRECTION ( 'NONE',  ( 1.000000000000000000, 0.000000000000000000, 0.000000000000000000 ) ) ;
#228306=PRODUCT_CONTEXT ( 'NONE', #225608, 'mechanical' ) ;
#228373=ORIENTED_EDGE ( 'NONE', *, *, #111590, .F. ) ;
#228651=DIRECTION ( 'NONE',  ( 0.000000000000000000, 6.982962677686266711E-15, -1.000000000000000000 ) ) ;
#228701=VERTEX_POINT ( 'NONE', #96012 ) ;
#228917=LINE ( 'NONE', #50253, #152623 ) ;
#228942=AXIS2_PLACEMENT_3D ( 'NONE', #209332, #129800, #11146 ) ;
#229105=ORIENTED_EDGE ( 'NONE', *, *, #167003, .F. ) ;
#229456=ORIENTED_EDGE ( 'NONE', *, *, #258025, .T. ) ;
#229626=EDGE_LOOP ( 'NONE', ( #24252, #220925, #152250, #219926, #10918, #34922, #238498, #191244, #45304, #119376, #173359, #243252, #137498, #115370 ) ) ;
#229647=CARTESIAN_POINT ( 'NONE',  ( 18.54999999999999716, 67.25000000001178080, -82.17310748452437963 ) ) ;
#229658=DIRECTION ( 'NONE',  ( 0.000000000000000000, 1.000000000000000000, 6.982962677686266711E-15 ) ) ;
#229780=EDGE_CURVE ( 'NONE', #228701, #51021, #66581, .T. ) ;
#229808=DIRECTION ( 'NONE',  ( -1.000000000000000000, -7.125593699324843413E-30, 1.020425574104004196E-15 ) ) ;
#229839=CARTESIAN_POINT ( 'NONE',  ( 13.54577453029515688, 66.54939790392327836, -84.57921152142770893 ) ) ;
#229888=CARTESIAN_POINT ( 'NONE',  ( -16.84419801905645997, 66.05000000001183480, -82.19259733074642327 ) ) ;
#229912=( BOUNDED_SURFACE ( )  B_SPLINE_SURFACE ( 3, 2, ( 
 ( #47753, #244676, #127312 ),
 ( #206850, #204264, #166471 ),
 ( #167750, #188565, #67336 ),
 ( #107743, #187302, #226385 ) ),
 .UNSPECIFIED., .F., .F., .F. ) 
 B_SPLINE_SURFACE_WITH_KNOTS ( ( 4, 4 ),
 ( 3, 3 ),
 ( 3.658908243880901523, 4.712388980384689674 ),
 ( 0.000000000000000000, 1.000000000000000000 ),
 .UNSPECIFIED. ) 
 GEOMETRIC_REPRESENTATION_ITEM ( )  RATIONAL_B_SPLINE_SURFACE ( (
 ( 1.000000000000000000, 0.8984936768950559927, 1.000000000000000000),
 ( 1.000000000000000000, 0.8646876308615171203, 1.000000000000000000),
 ( 1.000000000000000000, 0.7953136715913529109, 1.000000000000000000),
 ( 1.000000000000000000, 0.7071067811865475727, 1.000000000000000000) ) ) 
 REPRESENTATION_ITEM ( '' )  SURFACE ( )  );
#230018=CARTESIAN_POINT ( 'NONE',  ( 13.99999999999999822, 66.15000000001185754, -86.27310748452437394 ) ) ;
#230191=CARTESIAN_POINT ( 'NONE',  ( 14.87567385445976598, 66.56923500458952958, -87.79257008977393184 ) ) ;
#230294=VECTOR ( 'NONE', #28452, 1000.000000000000000 ) ;
#230327=DIRECTION ( 'NONE',  ( 0.8049926720990051576, -0.5932847527679298016, -4.142885285818778274E-15 ) ) ;
#230496=EDGE_CURVE ( 'NONE', #216777, #26102, #87489, .T. ) ;
#230715=CARTESIAN_POINT ( 'NONE',  ( -16.87036670365549895, 66.01058118071021852, -90.50266760182643111 ) ) ;
#230799=FACE_OUTER_BOUND ( 'NONE', #44387, .T. ) ;
#230913=CARTESIAN_POINT ( 'NONE',  ( 20.99999999999999645, 66.25000000001190870, -93.77310748452438816 ) ) ;
#231012=EDGE_CURVE ( 'NONE', #91289, #66229, #21027, .T. ) ;
#231129=VERTEX_POINT ( 'NONE', #144776 ) ;
#231206=CARTESIAN_POINT ( 'NONE',  ( -16.87036670365549895, 66.01058118071020431, -90.50266760182644532 ) ) ;
#231291=ORIENTED_EDGE ( 'NONE', *, *, #237414, .T. ) ;
#231341=ADVANCED_FACE ( 'NONE', ( #217581 ), #238454, .F. ) ;
#231436=CARTESIAN_POINT ( 'NONE',  ( 20.73486653747088582, 68.75000000001185185, -93.77310748452435973 ) ) ;
#231494=CARTESIAN_POINT ( 'NONE',  ( 13.12220780326572012, 66.56936653093907807, -87.79134168970030316 ) ) ;
#231635=FACE_OUTER_BOUND ( 'NONE', #134492, .T. ) ;
#231750=FACE_OUTER_BOUND ( 'NONE', #36701, .T. ) ;
#231832=CARTESIAN_POINT ( 'NONE',  ( -16.85939681242905763, 66.09477481408649169, -82.48318552933288572 ) ) ;
#231840=CARTESIAN_POINT ( 'NONE',  ( -16.88593481969334320, 66.04943990992750003, -82.17123522757988496 ) ) ;
#231882=CYLINDRICAL_SURFACE ( 'NONE', #255636, 0.09999999999999939493 ) ;
#232261=VERTEX_POINT ( 'NONE', #187843 ) ;
#232432=CARTESIAN_POINT ( 'NONE',  ( 12.60873083341396672, 66.61042836546540968, -85.20546677215523346 ) ) ;
#232620=VECTOR ( 'NONE', #213098, 1000.000000000000000 ) ;
#232697=VECTOR ( 'NONE', #90070, 1000.000000000000000 ) ;
#232781=CARTESIAN_POINT ( 'NONE',  ( 12.25000000000000178, 66.65000000001188596, -86.50158811269930936 ) ) ;
#232996=VECTOR ( 'NONE', #14060, 1000.000000000000000 ) ;
#233044=DIRECTION ( 'NONE',  ( 0.000000000000000000, 6.982962677686266711E-15, -1.000000000000000000 ) ) ;
#233157=VECTOR ( 'NONE', #47178, 1000.000000000000000 ) ;
#233394=CARTESIAN_POINT ( 'NONE',  ( -15.06774609480955363, 66.58234804117083172, -87.66432009208392628 ) ) ;
#233473=AXIS2_PLACEMENT_3D ( 'NONE', #123599, #186135, #67464 ) ;
#233534=AXIS2_PLACEMENT_3D ( 'NONE', #208074, #7273, #168973 ) ;
#233755=ORIENTED_EDGE ( 'NONE', *, *, #204543, .F. ) ;
#233884=EDGE_LOOP ( 'NONE', ( #242272, #156728, #18230, #92689, #120770, #40871, #125332, #250940, #146638 ) ) ;
#233900=ORIENTED_EDGE ( 'NONE', *, *, #154283, .F. ) ;
#233975=LINE ( 'NONE', #213132, #89252 ) ;
#234096=ORIENTED_EDGE ( 'NONE', *, *, #25918, .F. ) ;
#234119=CARTESIAN_POINT ( 'NONE',  ( -16.83794237512073622, 66.07364077890439091, -90.21956532582547084 ) ) ;
#234411=AXIS2_PLACEMENT_3D ( 'NONE', #222884, #44270, #2549 ) ;
#234452=LINE ( 'NONE', #55788, #180353 ) ;
#234512=EDGE_CURVE ( 'NONE', #103638, #10718, #195663, .T. ) ;
#234786=CARTESIAN_POINT ( 'NONE',  ( 23.24999999999999645, 67.17743825834548943, -93.77310748452437394 ) ) ;
#234801=CIRCLE ( 'NONE', #247246, 0.9000000000000014655 ) ;
#234952=AXIS2_PLACEMENT_3D ( 'NONE', #6020, #144240, #124707 ) ;
#235337=CARTESIAN_POINT ( 'NONE',  ( -16.93710578446424009, 66.05000000001187743, -90.10430350072498129 ) ) ;
#236175=VERTEX_POINT ( 'NONE', #126080 ) ;
#236184=ORIENTED_EDGE ( 'NONE', *, *, #10552, .F. ) ;
#236196=VERTEX_POINT ( 'NONE', #246053 ) ;
#236226=ORIENTED_EDGE ( 'NONE', *, *, #180172, .F. ) ;
#236316=CARTESIAN_POINT ( 'NONE',  ( -16.86445178670653888, 66.03778837089588194, -90.41388492264164256 ) ) ;
#236333=CARTESIAN_POINT ( 'NONE',  ( -18.40000000000000213, 64.66825945288670141, -90.37310748452438247 ) ) ;
#236471=DIRECTION ( 'NONE',  ( 0.000000000000000000, 1.000000000000000000, 6.982962677686266711E-15 ) ) ;
#236532=VECTOR ( 'NONE', #236471, 1000.000000000000000 ) ;
#236741=ORIENTED_EDGE ( 'NONE', *, *, #87499, .T. ) ;
#236761=ORIENTED_EDGE ( 'NONE', *, *, #154348, .T. ) ;
#236845=LINE ( 'NONE', #58193, #154250 ) ;
#236866=CARTESIAN_POINT ( 'NONE',  ( -14.45422546970484312, 66.54939790392329257, -84.57921152142773735 ) ) ;
#237246=CARTESIAN_POINT ( 'NONE',  ( -16.79184697841823493, 66.05123833835347114, -90.36896521392186798 ) ) ;
#237336=DIRECTION ( 'NONE',  ( 1.000000000000000000, 0.000000000000000000, 0.000000000000000000 ) ) ;
#237351=CARTESIAN_POINT ( 'NONE',  ( -18.40000000000000213, 70.35000000001181775, -82.17310748452435121 ) ) ;
#237414=EDGE_CURVE ( 'NONE', #255984, #245034, #39700, .T. ) ;
#237774=CARTESIAN_POINT ( 'NONE',  ( -16.94275863009466576, 66.01050395134947735, -90.41480486656550397 ) ) ;
#237913=CARTESIAN_POINT ( 'NONE',  ( -16.82542659449982736, 66.06550010858451571, -90.27847188449790394 ) ) ;
#237953=CARTESIAN_POINT ( 'NONE',  ( -16.87331047859651179, 66.05000000001187743, -90.37310748452438247 ) ) ;
#238222=EDGE_CURVE ( 'NONE', #64278, #65335, #245615, .T. ) ;
#238325=EDGE_CURVE ( 'NONE', #121302, #81650, #108667, .T. ) ;
#238454=PLANE ( 'NONE',  #190644 ) ;
#238497=CARTESIAN_POINT ( 'NONE',  ( -14.45443560709636266, 66.54940788787816075, -87.96691916571600700 ) ) ;
#238498=ORIENTED_EDGE ( 'NONE', *, *, #157873, .F. ) ;
#238536=ORIENTED_EDGE ( 'NONE', *, *, #244962, .F. ) ;
#238666=LINE ( 'NONE', #219085, #133793 ) ;
#238932=AXIS2_PLACEMENT_3D ( 'NONE', #198061, #22011, #101485 ) ;
#239181=ORIENTED_EDGE ( 'NONE', *, *, #216524, .T. ) ;
#239242=FACE_OUTER_BOUND ( 'NONE', #151436, .T. ) ;
#239495=FACE_OUTER_BOUND ( 'NONE', #6107, .T. ) ;
#239530=LINE ( 'NONE', #98683, #52477 ) ;
#239687=ADVANCED_FACE ( 'NONE', ( #139818 ), #138514, .F. ) ;
#239775=CARTESIAN_POINT ( 'NONE',  ( -16.88560720703333473, 66.04943515626217732, -90.37499556366066145 ) ) ;
#239938=ORIENTED_EDGE ( 'NONE', *, *, #250997, .T. ) ;
#240319=ORIENTED_EDGE ( 'NONE', *, *, #231012, .F. ) ;
#240447=CARTESIAN_POINT ( 'NONE',  ( -16.77828822459933633, 66.05377062495534801, -82.18573573544333044 ) ) ;
#240464=CARTESIAN_POINT ( 'NONE',  ( -16.87683809663752044, 66.05000000001182059, -82.92547150272069700 ) ) ;
#240730=CARTESIAN_POINT ( 'NONE',  ( -15.57281606413133979, 66.62934494888835957, -85.49728422854349219 ) ) ;
#240966=CARTESIAN_POINT ( 'NONE',  ( -18.34374000495059676, 64.52683809664929981, -78.77310748452438816 ) ) ;
#240978=ORIENTED_EDGE ( 'NONE', *, *, #8314, .F. ) ;
#241071=CARTESIAN_POINT ( 'NONE',  ( -16.89268316805466341, 66.04827818676967865, -90.37885996306994230 ) ) ;
#241191=DIRECTION ( 'NONE',  ( -0.000000000000000000, -6.982962677686266711E-15, 1.000000000000000000 ) ) ;
#241494=VECTOR ( 'NONE', #214402, 1000.000000000000000 ) ;
#241497=DIRECTION ( 'NONE',  ( 1.000000000000000000, 0.000000000000000000, 0.000000000000000000 ) ) ;
#241570=EDGE_CURVE ( 'NONE', #86629, #91289, #63421, .T. ) ;
#241594=DIRECTION ( 'NONE',  ( 1.000000000000000000, 0.000000000000000000, 0.000000000000000000 ) ) ;
#241608=VECTOR ( 'NONE', #134269, 1000.000000000000000 ) ;
#241646=CARTESIAN_POINT ( 'NONE',  ( -16.85718274719363308, 66.02385768539012645, -82.08645381670704921 ) ) ;
#241745=EDGE_LOOP ( 'NONE', ( #147726, #23862, #215354, #84485 ) ) ;
#241762=CARTESIAN_POINT ( 'NONE',  ( -16.80891096016328135, 66.05000000001187743, -90.39077029179252065 ) ) ;
#241858=ORIENTED_EDGE ( 'NONE', *, *, #208611, .F. ) ;
#241926=CARTESIAN_POINT ( 'NONE',  ( -18.39999999999999858, 64.52683809664941350, -93.69716141771641560 ) ) ;
#241961=EDGE_CURVE ( 'NONE', #189338, #225448, #18585, .T. ) ;
#242272=ORIENTED_EDGE ( 'NONE', *, *, #3065, .F. ) ;
#242526=CARTESIAN_POINT ( 'NONE',  ( -17.11825945287481332, 66.05000000001182059, -82.27310748452437394 ) ) ;
#242539=AXIS2_PLACEMENT_3D ( 'NONE', #169279, #87117, #208386 ) ;
#242654=CARTESIAN_POINT ( 'NONE',  ( -16.97048326478264713, 66.05000000001187743, -89.88200060439721994 ) ) ;
#242753=ORIENTED_EDGE ( 'NONE', *, *, #196250, .T. ) ;
#242876=DIRECTION ( 'NONE',  ( 1.186688945009010077E-16, 1.000000000000000000, 6.982962677686266711E-15 ) ) ;
#242922=CARTESIAN_POINT ( 'NONE',  ( -16.94878442675511465, 66.00827089702079320, -82.13488790888651181 ) ) ;
#243196=DIRECTION ( 'NONE',  ( -0.7071067811865487940, -0.7071067811865463515, -4.937700262164522799E-15 ) ) ;
#243201=ORIENTED_EDGE ( 'NONE', *, *, #149391, .F. ) ;
#243252=ORIENTED_EDGE ( 'NONE', *, *, #211451, .T. ) ;
#243343=EDGE_CURVE ( 'NONE', #161815, #169411, #187976, .T. ) ;
#243349=CARTESIAN_POINT ( 'NONE',  ( 18.39999999999999503, 64.25000000001188027, -90.37310748452439668 ) ) ;
#243372=ORIENTED_EDGE ( 'NONE', *, *, #60851, .F. ) ;
#243728=ORIENTED_EDGE ( 'NONE', *, *, #50610, .T. ) ;
#244676=CARTESIAN_POINT ( 'NONE',  ( -16.91049119928363709, 66.05000000001183480, -82.14138709133354155 ) ) ;
#244962=EDGE_CURVE ( 'NONE', #14013, #81650, #221971, .T. ) ;
#245034=VERTEX_POINT ( 'NONE', #219415 ) ;
#245324=VECTOR ( 'NONE', #60261, 1000.000000000000000 ) ;
#245615=LINE ( 'NONE', #66971, #135876 ) ;
#245735=EDGE_LOOP ( 'NONE', ( #152463, #145334 ) ) ;
#245747=ADVANCED_FACE ( 'NONE', ( #185289 ), #45768, .T. ) ;
#245911=CYLINDRICAL_SURFACE ( 'NONE', #228942, 1.500000000000001332 ) ;
#246053=CARTESIAN_POINT ( 'NONE',  ( -21.65000000000000213, 66.05000000001182059, -82.27310748452437394 ) ) ;
#246216=VECTOR ( 'NONE', #228651, 1000.000000000000000 ) ;
#246233=CARTESIAN_POINT ( 'NONE',  ( 18.39999999999998082, 64.52683809664941350, -93.77310748452438816 ) ) ;
#246309=EDGE_CURVE ( 'NONE', #215091, #26497, #150992, .T. ) ;
#246430=EDGE_LOOP ( 'NONE', ( #145699, #40070, #147870 ) ) ;
#246510=CARTESIAN_POINT ( 'NONE',  ( -16.81744102076749314, 66.05000000001187743, -90.37310748452438247 ) ) ;
#247202=DIRECTION ( 'NONE',  ( -1.000000000000000000, 0.000000000000000000, -0.000000000000000000 ) ) ;
#247246=AXIS2_PLACEMENT_3D ( 'NONE', #110618, #34977, #132773 ) ;
#247360=DIRECTION ( 'NONE',  ( -1.000000000000000000, 0.000000000000000000, 0.000000000000000000 ) ) ;
#247411=VECTOR ( 'NONE', #180581, 1000.000000000000000 ) ;
#247441=VERTEX_POINT ( 'NONE', #3813 ) ;
#247637=ORIENTED_EDGE ( 'NONE', *, *, #100259, .T. ) ;
#247988=ORIENTED_EDGE ( 'NONE', *, *, #210966, .T. ) ;
#248112=CARTESIAN_POINT ( 'NONE',  ( 12.30626653967340722, 66.64320997496595567, -85.81828097591049698 ) ) ;
#248479=CARTESIAN_POINT ( 'NONE',  ( 13.76927104934457446, 66.54401276639910634, -88.01157631762656308 ) ) ;
#248609=EDGE_LOOP ( 'NONE', ( #197903, #206862 ) ) ;
#249107=EDGE_LOOP ( 'NONE', ( #89796, #153987, #164409, #30446 ) ) ;
#249144=EDGE_CURVE ( 'NONE', #201406, #217324, #145155, .T. ) ;
#249247=VERTEX_POINT ( 'NONE', #28219 ) ;
#249415=CARTESIAN_POINT ( 'NONE',  ( 15.07585980824113392, 66.58236703690555203, -84.87415901879209912 ) ) ;
#249611=DIRECTION ( 'NONE',  ( 1.000000000000000000, -1.186688945009010077E-16, -8.286604613020808509E-31 ) ) ;
#249740=CARTESIAN_POINT ( 'NONE',  ( -18.40000000000000213, 64.52683809664938508, -90.47310748452439100 ) ) ;
#249761=CARTESIAN_POINT ( 'NONE',  ( 14.77516762759920788, 66.56332574816902081, -87.84624555352516495 ) ) ;
#249780=CARTESIAN_POINT ( 'NONE',  ( -16.93521499325732549, 66.00521388020827374, -82.11599894343083861 ) ) ;
#249818=ADVANCED_FACE ( 'NONE', ( #210378 ), #13268, .T. ) ;
#250012=VECTOR ( 'NONE', #224566, 1000.000000000000000 ) ;
#250050=LINE ( 'NONE', #71432, #44576 ) ;
#250100=CARTESIAN_POINT ( 'NONE',  ( -16.78493211734302903, 66.05416425680760995, -82.18705650362834092 ) ) ;
#250123=DIRECTION ( 'NONE',  ( -1.000000000000000000, 0.000000000000000000, 0.000000000000000000 ) ) ;
#250430=ADVANCED_FACE ( 'NONE', ( #40447 ), #22151, .F. ) ;
#250487=LINE ( 'NONE', #234786, #128355 ) ;
#250569=LINE ( 'NONE', #51055, #125970 ) ;
#250643=CARTESIAN_POINT ( 'NONE',  ( -17.27223548804785125, 65.65460260859495634, -91.65671366372575335 ) ) ;
#250940=ORIENTED_EDGE ( 'NONE', *, *, #75642, .F. ) ;
#250997=EDGE_CURVE ( 'NONE', #236196, #69522, #184722, .T. ) ;
#251045=CARTESIAN_POINT ( 'NONE',  ( -16.93826681692523550, 65.98857127972409842, -82.07764901716494421 ) ) ;
#251100=DIRECTION ( 'NONE',  ( -0.000000000000000000, -6.982962677686266711E-15, 1.000000000000000000 ) ) ;
#251465=DIRECTION ( 'NONE',  ( -0.8049926720990042694, 0.5932847527679310229, 4.142885285818786163E-15 ) ) ;
#251510=DIRECTION ( 'NONE',  ( -1.073024830501117725E-15, 6.982962677686266711E-15, -1.000000000000000000 ) ) ;
#252059=CARTESIAN_POINT ( 'NONE',  ( -16.87242674293850087, 66.05000000001189164, -90.37419773089673924 ) ) ;
#252101=DIRECTION ( 'NONE',  ( 1.073024830501117725E-15, 6.982962677686266711E-15, -1.000000000000000000 ) ) ;
#252307=CARTESIAN_POINT ( 'NONE',  ( 12.25000000000000000, 66.65000000001185754, -86.27310748452437394 ) ) ;
#252448=PLANE ( 'NONE',  #105251 ) ;
#252453=AXIS2_PLACEMENT_3D ( 'NONE', #123552, #103957, #4848 ) ;
#252624=CIRCLE ( 'NONE', #35629, 0.09999999999999516220 ) ;
#252644=CARTESIAN_POINT ( 'NONE',  ( -16.87683809663752399, 66.13508655273160741, -82.79882593322042794 ) ) ;
#252687=CARTESIAN_POINT ( 'NONE',  ( -16.97683809663752186, 66.15000000001188596, -90.37310748452438247 ) ) ;
#252846=ORIENTED_EDGE ( 'NONE', *, *, #12047, .F. ) ;
#252945=AXIS2_PLACEMENT_3D ( 'NONE', #38471, #138810, #81413 ) ;
#253194=VERTEX_POINT ( 'NONE', #60714 ) ;
#253591=CARTESIAN_POINT ( 'NONE',  ( 14.22821877134046176, 66.54397173950393096, -88.01190944945867045 ) ) ;
#253609=CARTESIAN_POINT ( 'NONE',  ( -16.93353400591625757, 65.99538760383886427, -82.09042301431897215 ) ) ;
#253675=CARTESIAN_POINT ( 'NONE',  ( -16.87683809663753109, 66.13508622147344340, -89.74739184888585442 ) ) ;
#254188=CARTESIAN_POINT ( 'NONE',  ( -16.81744102076749314, 66.05000000001187743, -90.37310748452438247 ) ) ;
#254275=LINE ( 'NONE', #78217, #186898 ) ;
#254626=ORIENTED_EDGE ( 'NONE', *, *, #196250, .F. ) ;
#254851=CARTESIAN_POINT ( 'NONE',  ( -16.87683809663752399, 66.15000000001190017, -89.62074346632789457 ) ) ;
#254867=ADVANCED_FACE ( 'NONE', ( #73343 ), #74638, .F. ) ;
#255018=EDGE_LOOP ( 'NONE', ( #128107, #17822, #214004, #219945 ) ) ;
#255105=EDGE_CURVE ( 'NONE', #153574, #111618, #186104, .T. ) ;
#255443=CARTESIAN_POINT ( 'NONE',  ( -12.47155713865592297, 66.62433047358608462, -87.15531747513844607 ) ) ;
#255636=AXIS2_PLACEMENT_3D ( 'NONE', #252687, #152354, #156201 ) ;
#255646=EDGE_LOOP ( 'NONE', ( #24303, #146001, #48516, #164664 ) ) ;
#255834=CARTESIAN_POINT ( 'NONE',  ( -16.94107738177415712, 65.98576071487524075, -90.47310748452439100 ) ) ;
#255929=CARTESIAN_POINT ( 'NONE',  ( -18.40000000000000213, 70.35000000001181775, -82.17310748452435121 ) ) ;
#255984=VERTEX_POINT ( 'NONE', #140357 ) ;
#256040=ADVANCED_FACE ( 'NONE', ( #74680 ), #211590, .T. ) ;
#256170=CARTESIAN_POINT ( 'NONE',  ( -16.98495255085918032, 65.99443563401710833, -90.38849027830387683 ) ) ;
#256187=CARTESIAN_POINT ( 'NONE',  ( -16.81930730667006557, 66.06300193113784758, -90.29633975398620294 ) ) ;
#256463=( BOUNDED_CURVE ( )  B_SPLINE_CURVE ( 3, ( #111522, #191082, #106359, #185919 ),
 .UNSPECIFIED., .F., .F. ) 
 B_SPLINE_CURVE_WITH_KNOTS ( ( 4, 4 ),
 ( -9.769962616701377556E-15, 1.570796326794793529 ),
 .UNSPECIFIED. ) 
 CURVE ( )  GEOMETRIC_REPRESENTATION_ITEM ( )  RATIONAL_B_SPLINE_CURVE ( ( 1.000000000000000000, 0.8047378541243870309, 0.8047378541243870309, 1.000000000000000000 ) ) 
 REPRESENTATION_ITEM ( '' )  );
#256590=CARTESIAN_POINT ( 'NONE',  ( -21.64999999999999858, 65.95000000001181206, -82.17310748452439384 ) ) ;
#256727=CARTESIAN_POINT ( 'NONE',  ( -15.70407651835961005, 66.64419340838171024, -86.73200495297821533 ) ) ;
#256733=ORIENTED_EDGE ( 'NONE', *, *, #225891, .F. ) ;
#256860=EDGE_CURVE ( 'NONE', #209659, #100827, #141856, .T. ) ;
#256928=CARTESIAN_POINT ( 'NONE',  ( -16.27683809663750480, 66.65000000001191438, -93.77310748452437394 ) ) ;
#256979=VERTEX_POINT ( 'NONE', #150851 ) ;
#257124=VERTEX_POINT ( 'NONE', #195143 ) ;
#257256=ORIENTED_EDGE ( 'NONE', *, *, #46866, .T. ) ;
#257324=ORIENTED_EDGE ( 'NONE', *, *, #92959, .F. ) ;
#257393=FACE_OUTER_BOUND ( 'NONE', #140375, .T. ) ;
#257418=CARTESIAN_POINT ( 'NONE',  ( -16.83233564386414116, 66.06977820342717678, -90.24762814800000399 ) ) ;
#257482=CARTESIAN_POINT ( 'NONE',  ( -16.77683809663752257, 66.05416425680770942, -90.35915846542016538 ) ) ;
#257652=CARTESIAN_POINT ( 'NONE',  ( -12.42749937872396515, 66.62931007840923314, -85.49664235786333677 ) ) ;
#257674=LINE ( 'NONE', #140344, #227577 ) ;
#257837=B_SPLINE_CURVE_WITH_KNOTS ( 'NONE', 3,
 ( #203647, #25037, #131806, #146227 ),
 .UNSPECIFIED., .F., .F.,
 ( 4, 4 ),
 ( 0.000000000000000000, 7.713889350928753320E-05 ),
 .UNSPECIFIED. ) ;
#257965=DIRECTION ( 'NONE',  ( 0.000000000000000000, -6.982962677686266711E-15, 1.000000000000000000 ) ) ;
#258025=EDGE_CURVE ( 'NONE', #148732, #153574, #191511, .T. ) ;
ENDSEC;
END-ISO-10303-21;
